ISO-10303-21;
HEADER;
FILE_DESCRIPTION (('STEP AP214'),
    '1' );
FILE_NAME ('Snap Open Cable Crossbars 7.step',
    '2026-10-08T22:59:04',
    ( '' ),
    ( '' ),
    'SwSTEP 2.0',
    'SolidWorks 2020',
    '' );
FILE_SCHEMA (( 'AUTOMOTIVE_DESIGN' ));
ENDSEC;

DATA;
#108=CARTESIAN_POINT ( 'NONE',  ( -16.82055514392371620, 14.15329893112338588, -219.2288882764422624 ) ) ;
#134=CARTESIAN_POINT ( 'NONE',  ( -16.93909480342660245, 12.44555890197899295, -211.1852061227702109 ) ) ;
#279=VECTOR ( 'NONE', #178302, 1000.000000000000227 ) ;
#303=DIRECTION ( 'NONE',  ( 0.7071067811865462405, 0.6909108974501247946, 0.1504730267678065503 ) ) ;
#337=CARTESIAN_POINT ( 'NONE',  ( -23.25000000000000355, 7.488999128699433072, -208.8358083214519070 ) ) ;
#353=ADVANCED_FACE ( 'NONE', ( #239625 ), #221311, .T. ) ;
#356=EDGE_LOOP ( 'NONE', ( #15486, #102274, #95283, #141475 ) ) ;
#696=VECTOR ( 'NONE', #239567, 1000.000000000000227 ) ;
#976=CARTESIAN_POINT ( 'NONE',  ( -16.97683809663753962, 14.02673956256705523, -218.6477791648082700 ) ) ;
#1053=CARTESIAN_POINT ( 'NONE',  ( -16.94107738177414291, 14.24304960796391306, -219.3391119284832484 ) ) ;
#1114=CARTESIAN_POINT ( 'NONE',  ( -15.52965525596988527, 12.53792204840291369, -214.5112614470118615 ) ) ;
#1385=CARTESIAN_POINT ( 'NONE',  ( -16.97683809663752186, 13.99889777621145903, -218.5199410132753428 ) ) ;
#1395=( BOUNDED_SURFACE ( )  B_SPLINE_SURFACE ( 3, 2, ( 
 ( #95052, #196717, #256638 ),
 ( #59750, #15551, #178476 ),
 ( #54636, #115915, #134173 ),
 ( #179742, #114620, #156350 ),
 ( #254115, #75520, #155065 ),
 ( #234564, #74250, #117193 ),
 ( #199305, #55900, #237139 ),
 ( #177196, #135452, #20676 ),
 ( #217549, #37676, #98873 ),
 ( #235840, #38951, #214996 ) ),
 .UNSPECIFIED., .F., .F., .F. ) 
 B_SPLINE_SURFACE_WITH_KNOTS ( ( 4, 2, 2, 2, 4 ),
 ( 3, 3 ),
 ( 0.002161241639767768653, 0.002579950749617439427, 0.002789305304542274815, 0.002893982582004692508, 0.002998659859467110202 ),
 ( 0.000000000000000000, 1.000000000000000000 ),
 .UNSPECIFIED. ) 
 GEOMETRIC_REPRESENTATION_ITEM ( )  RATIONAL_B_SPLINE_SURFACE ( (
 ( 1.000000000000000000, 0.7071067811864816255, 1.000000000000000000),
 ( 1.000000000000000000, 0.7632447400665326454, 1.000000000000000000),
 ( 1.000000000000000000, 0.8158073005107645548, 1.000000000000000000),
 ( 1.000000000000000000, 0.8906973462396717833, 1.000000000000000000),
 ( 1.000000000000000000, 0.9149408947796511260, 1.000000000000000000),
 ( 1.000000000000000000, 0.9493368785277698230, 1.000000000000000000),
 ( 1.000000000000000000, 0.9605194247158244103, 1.000000000000000000),
 ( 1.000000000000000000, 0.9803630264779819026, 1.000000000000000000),
 ( 1.000000000000000000, 0.9900844824272359013, 1.000000000000000000),
 ( 1.000000000000000000, 0.9894588281429361754, 1.000000000000000000) ) ) 
 REPRESENTATION_ITEM ( '' )  SURFACE ( )  );
#1397=VECTOR ( 'NONE', #170639, 1000.000000000000227 ) ;
#1520=ORIENTED_EDGE ( 'NONE', *, *, #63237, .F. ) ;
#1583=CARTESIAN_POINT ( 'NONE',  ( 15.48841904831874849, 12.80238349835111755, -219.5505295114098772 ) ) ;
#1650=ORIENTED_EDGE ( 'NONE', *, *, #170622, .T. ) ;
#1738=CARTESIAN_POINT ( 'NONE',  ( -16.81744102076748959, 14.15900158805613884, -219.2550725561364118 ) ) ;
#1955=ADVANCED_FACE ( 'NONE', ( #65835 ), #8446, .F. ) ;
#2298=CYLINDRICAL_SURFACE ( 'NONE', #45055, 1.749999999999999778 ) ;
#2357=DIRECTION ( 'NONE',  ( 0.000000000000000000, -0.9770955615653313941, -0.2128009952263603677 ) ) ;
#2425=AXIS2_PLACEMENT_3D ( 'NONE', #153513, #135160, #16531 ) ;
#2478=CARTESIAN_POINT ( 'NONE',  ( -17.11825945287481332, 14.13772148853350252, -219.1573629999798811 ) ) ;
#2676=CARTESIAN_POINT ( 'NONE',  ( -16.87683809663752399, 13.90118822005493016, -218.5412211127979845 ) ) ;
#2838=CARTESIAN_POINT ( 'NONE',  ( -17.11825945287481332, 14.25671114421267127, -219.2337924566137701 ) ) ;
#2857=ORIENTED_EDGE ( 'NONE', *, *, #93165, .F. ) ;
#3018=CARTESIAN_POINT ( 'NONE',  ( -16.80117486205003630, 14.15842302226418958, -219.2540265911986808 ) ) ;
#3138=CARTESIAN_POINT ( 'NONE',  ( -21.65000000000000213, 11.52084357182974372, -219.8296352432475942 ) ) ;
#3309=CARTESIAN_POINT ( 'NONE',  ( -16.92973740335258270, 14.21246129500415734, -219.3008027365993087 ) ) ;
#3390=CARTESIAN_POINT ( 'NONE',  ( -17.27223548800067121, 14.81849529660560449, -220.4251374982360403 ) ) ;
#3415=CARTESIAN_POINT ( 'NONE',  ( -16.89268316805466341, 12.41449167011727361, -211.2369018264743090 ) ) ;
#3665=ORIENTED_EDGE ( 'NONE', *, *, #11859, .T. ) ;
#3791=AXIS2_PLACEMENT_3D ( 'NONE', #250887, #113949, #197334 ) ;
#3891=VERTEX_POINT ( 'NONE', #14024 ) ;
#4057=CARTESIAN_POINT ( 'NONE',  ( 18.54999999999999716, 14.15900158805616371, -219.2550725561364686 ) ) ;
#4209=CARTESIAN_POINT ( 'NONE',  ( -16.87036670365549895, 12.42497885867826390, -211.1079079717509046 ) ) ;
#4263=VECTOR ( 'NONE', #56005, 1000.000000000000227 ) ;
#4387=DIRECTION ( 'NONE',  ( 1.000000000000000000, 0.000000000000000000, 0.000000000000000000 ) ) ;
#4462=( BOUNDED_SURFACE ( )  B_SPLINE_SURFACE ( 3, 2, ( 
 ( #12331, #73595, #13599 ),
 ( #14894, #112695, #133536 ),
 ( #38300, #137372, #215627 ),
 ( #177827, #37030, #16183 ) ),
 .UNSPECIFIED., .F., .F., .F. ) 
 B_SPLINE_SURFACE_WITH_KNOTS ( ( 4, 4 ),
 ( 3, 3 ),
 ( 3.658908243880901523, 4.712388980384689674 ),
 ( 0.000000000000000000, 1.000000000000000000 ),
 .UNSPECIFIED. ) 
 GEOMETRIC_REPRESENTATION_ITEM ( )  RATIONAL_B_SPLINE_SURFACE ( (
 ( 1.000000000000000000, 0.8984936768950373409, 1.000000000000000000),
 ( 1.000000000000000000, 0.8646876308614469542, 1.000000000000000000),
 ( 1.000000000000000000, 0.7953136715914278509, 1.000000000000000000),
 ( 1.000000000000000000, 0.7071067811863926966, 1.000000000000000000) ) ) 
 REPRESENTATION_ITEM ( '' )  SURFACE ( )  );
#4710=ORIENTED_EDGE ( 'NONE', *, *, #63243, .F. ) ;
#4733=DIRECTION ( 'NONE',  ( -1.073024830501117725E-15, 0.2128009952263604232, -0.9770955615653316162 ) ) ;
#5085=CARTESIAN_POINT ( 'NONE',  ( -12.92414019175887141, 13.06404166453377336, -216.7291753257208313 ) ) ;
#5445=ADVANCED_FACE ( 'NONE', ( #76269 ), #155842, .F. ) ;
#5535=CARTESIAN_POINT ( 'NONE',  ( -16.90128866880176162, 14.16540792955462713, -219.2666506534965833 ) ) ;
#5565=ORIENTED_EDGE ( 'NONE', *, *, #214767, .F. ) ;
#5838=ADVANCED_FACE ( 'NONE', ( #230777 ), #190369, .F. ) ;
#5954=CARTESIAN_POINT ( 'NONE',  ( -16.94107738177414291, 14.24304960796391661, -219.3391119284832484 ) ) ;
#6595=AXIS2_PLACEMENT_3D ( 'NONE', #16166, #39589, #196065 ) ;
#6693=CARTESIAN_POINT ( 'NONE',  ( -16.78493832629887450, 12.41293291551535916, -211.2574046339461802 ) ) ;
#6707=DIRECTION ( 'NONE',  ( 0.000000000000000000, -0.2128009952263603677, 0.9770955615653313941 ) ) ;
#6910=AXIS2_PLACEMENT_3D ( 'NONE', #46230, #188318, #67089 ) ;
#7201=SURFACE_SIDE_STYLE ('',( #51450 ) ) ;
#7330=CARTESIAN_POINT ( 'NONE',  ( 21.13736287352038445, 12.29923930194942372, -219.6601089527135571 ) ) ;
#7503=CIRCLE ( 'NONE', #140795, 1.749999999999998002 ) ;
#7538=CARTESIAN_POINT ( 'NONE',  ( -16.89208623190940273, 14.16166532508835729, -219.2598882133882512 ) ) ;
#7651=CARTESIAN_POINT ( 'NONE',  ( 18.39999999999999503, 15.91777359887373500, -218.8720307647289758 ) ) ;
#7704=CARTESIAN_POINT ( 'NONE',  ( -12.26136940704872380, 12.75047551130877288, -215.6006359250795867 ) ) ;
#7910=VECTOR ( 'NONE', #242891, 1000.000000000000227 ) ;
#8017=DIRECTION ( 'NONE',  ( -0.7071067811865487940, 0.6909108974501226852, 0.1504730267678046352 ) ) ;
#8386=ORIENTED_EDGE ( 'NONE', *, *, #120907, .T. ) ;
#8427=EDGE_LOOP ( 'NONE', ( #194193, #49145, #32701, #63973 ) ) ;
#8446=CYLINDRICAL_SURFACE ( 'NONE', #217872, 0.1000000000000013656 ) ;
#8828=CARTESIAN_POINT ( 'NONE',  ( -16.89081410710458542, 14.16122750184362644, -219.2590969763894293 ) ) ;
#8972=CARTESIAN_POINT ( 'NONE',  ( -14.87770893841226894, 13.10213769539062234, -216.8429874065679428 ) ) ;
#9150=ORIENTED_EDGE ( 'NONE', *, *, #97280, .F. ) ;
#9255=EDGE_LOOP ( 'NONE', ( #250165, #202311 ) ) ;
#9271=CARTESIAN_POINT ( 'NONE',  ( -23.25000000000000355, 13.44928205424795564, -207.5377222505711075 ) ) ;
#9291=CARTESIAN_POINT ( 'NONE',  ( -18.34374000495059676, 16.37079970714665933, -222.2530670965321349 ) ) ;
#9476=PLANE ( 'NONE',  #248521 ) ;
#9763=VECTOR ( 'NONE', #303, 1000.000000000000114 ) ;
#9783=( NAMED_UNIT ( * ) PLANE_ANGLE_UNIT ( ) SI_UNIT ( $, .RADIAN. ) );
#9942=ORIENTED_EDGE ( 'NONE', *, *, #135217, .T. ) ;
#10035=CARTESIAN_POINT ( 'NONE',  ( -16.85939681242905408, 14.04926739942075997, -218.9616247998112328 ) ) ;
#10271=PLANE ( 'NONE',  #186820 ) ;
#10324=CARTESIAN_POINT ( 'NONE',  ( -18.41431012584568805, 13.18782249248739369, -207.5708846587602920 ) ) ;
#10426=CARTESIAN_POINT ( 'NONE',  ( -18.37160782347004329, 13.18118307098499820, -207.5961113505749438 ) ) ;
#10700=ORIENTED_EDGE ( 'NONE', *, *, #28842, .F. ) ;
#10814=EDGE_LOOP ( 'NONE', ( #232329, #22052, #45587, #225074, #73174 ) ) ;
#11077=SURFACE_STYLE_USAGE ( .BOTH. , #7201 ) ;
#11216=ORIENTED_EDGE ( 'NONE', *, *, #178228, .F. ) ;
#11324=CARTESIAN_POINT ( 'NONE',  ( -16.87683809663752044, 13.94271038643071670, -218.6617923402251336 ) ) ;
#11396=ORIENTED_EDGE ( 'NONE', *, *, #153924, .F. ) ;
#11456=LINE ( 'NONE', #250052, #192519 ) ;
#11482=CARTESIAN_POINT ( 'NONE',  ( -33.72168855820451938, 14.15900158805616726, -219.2550725561364686 ) ) ;
#11514=EDGE_CURVE ( 'NONE', #94156, #135298, #122031, .T. ) ;
#11605=CARTESIAN_POINT ( 'NONE',  ( -18.44085059012131822, 13.22076274678546248, -207.5974132564758747 ) ) ;
#11608=VECTOR ( 'NONE', #121140, 1000.000000000000000 ) ;
#11733=CARTESIAN_POINT ( 'NONE',  ( -14.00000000000000178, 13.18880795147152440, -215.2702608532411830 ) ) ;
#11819=ADVANCED_FACE ( 'NONE', ( #48060 ), #127610, .F. ) ;
#11859=EDGE_CURVE ( 'NONE', #196416, #119125, #91046, .T. ) ;
#11868=CARTESIAN_POINT ( 'NONE',  ( -17.71734398241073905, 12.78051993042367585, -208.7322573998702353 ) ) ;
#11947=CARTESIAN_POINT ( 'NONE',  ( 18.54999999999999716, 12.98648691417778167, -219.5104337504080263 ) ) ;
#12093=LINE ( 'NONE', #32959, #142833 ) ;
#12158=EDGE_LOOP ( 'NONE', ( #62416, #136439, #88320, #191658, #154857, #215888, #77129, #33848, #98345, #223296, #5565, #47566, #1520, #253492 ) ) ;
#12331=CARTESIAN_POINT ( 'NONE',  ( -16.87242674293849731, 14.15923359356921729, -219.2561378310278144 ) ) ;
#12775=DIRECTION ( 'NONE',  ( 1.000000000000000000, 0.000000000000000000, 0.000000000000000000 ) ) ;
#12892=EDGE_CURVE ( 'NONE', #210898, #21362, #21196, .T. ) ;
#13040=EDGE_LOOP ( 'NONE', ( #185620, #9150, #193775, #47801, #69019, #142300, #89579, #227387, #45635, #199314, #58093, #75285 ) ) ;
#13149=CARTESIAN_POINT ( 'NONE',  ( 15.66039659514496130, 12.83090422469976488, -215.9260128953783351 ) ) ;
#13483=ORIENTED_EDGE ( 'NONE', *, *, #127764, .T. ) ;
#13599=CARTESIAN_POINT ( 'NONE',  ( -16.93388492042257809, 14.20741668428894222, -219.2962582334711499 ) ) ;
#13975=CARTESIAN_POINT ( 'NONE',  ( -18.40000000000000213, 16.35463830854640932, -222.1788605317357224 ) ) ;
#14024=CARTESIAN_POINT ( 'NONE',  ( -18.40000000000000213, 16.64129698264336099, -222.1941556740511032 ) ) ;
#14149=ADVANCED_FACE ( 'NONE', ( #226763 ), #49419, .F. ) ;
#14157=PRODUCT_DEFINITION_CONTEXT ( 'detailed design', #179206, 'design' ) ;
#14199=CARTESIAN_POINT ( 'NONE',  ( -14.00000000000000178, 13.18880795147152440, -215.2702608532411830 ) ) ;
#14894=CARTESIAN_POINT ( 'NONE',  ( -16.92209698673895701, 14.14609827904097017, -219.1958258126950909 ) ) ;
#15353=CARTESIAN_POINT ( 'NONE',  ( -16.94445028196807002, 14.20918193489391790, -219.2878138714100373 ) ) ;
#15486=ORIENTED_EDGE ( 'NONE', *, *, #117947, .F. ) ;
#15551=CARTESIAN_POINT ( 'NONE',  ( -16.89155683852503387, 12.54753878115997701, -211.8558912009372932 ) ) ;
#15616=VERTEX_POINT ( 'NONE', #230340 ) ;
#15718=EDGE_CURVE ( 'NONE', #78646, #76812, #133805, .T. ) ;
#15736=CARTESIAN_POINT ( 'NONE',  ( 15.57250062127603485, 12.88570875296796814, -216.1309391439169190 ) ) ;
#15895=CARTESIAN_POINT ( 'NONE',  ( -16.93302609847409457, 12.44611011958480518, -211.1708003455683524 ) ) ;
#15935=ORIENTED_EDGE ( 'NONE', *, *, #151014, .T. ) ;
#16129=EDGE_CURVE ( 'NONE', #55330, #42401, #252160, .T. ) ;
#16144=EDGE_CURVE ( 'NONE', #169097, #22978, #43403, .T. ) ;
#16166=CARTESIAN_POINT ( 'NONE',  ( 20.04999999999999716, 10.51799536955199166, -208.1761252362501864 ) ) ;
#16183=CARTESIAN_POINT ( 'NONE',  ( -17.11825945287481687, 14.25671114421267305, -219.2337924566137701 ) ) ;
#16359=CARTESIAN_POINT ( 'NONE',  ( -17.11825945287481332, 14.25671114421267127, -219.2337924566137701 ) ) ;
#16373=DIRECTION ( 'NONE',  ( -1.000000000000000000, 0.000000000000000000, 0.000000000000000000 ) ) ;
#16531=DIRECTION ( 'NONE',  ( 1.000000000000000000, 0.000000000000000000, 0.000000000000000000 ) ) ;
#16545=CARTESIAN_POINT ( 'NONE',  ( 13.76927104934457624, 12.43387192838033251, -213.6554569813165472 ) ) ;
#16750=CARTESIAN_POINT ( 'NONE',  ( -16.86133551771148475, 14.14864742250337137, -219.2075304419909116 ) ) ;
#17169=CARTESIAN_POINT ( 'NONE',  ( -16.94180778212363236, 12.44575456678690806, -211.1890899969216946 ) ) ;
#17273=VERTEX_POINT ( 'NONE', #168609 ) ;
#17794=CARTESIAN_POINT ( 'NONE',  ( 15.52844286134407881, 12.53760658702568165, -214.5091953838863219 ) ) ;
#17989=CARTESIAN_POINT ( 'NONE',  ( -21.65000000000000213, 12.43531352672262180, -211.3405985074572300 ) ) ;
#18272=CARTESIAN_POINT ( 'NONE',  ( 13.22461703343585171, 13.11968191886198554, -216.8952266020228592 ) ) ;
#18400=CARTESIAN_POINT ( 'NONE',  ( -16.85722902420155123, 14.13441297064198743, -219.1421716323650344 ) ) ;
#18430=CARTESIAN_POINT ( 'NONE',  ( -16.93772744219065984, 12.44552478725261757, -211.1828749433600478 ) ) ;
#18458=DIRECTION ( 'NONE',  ( -0.000000000000000000, 0.2128009952263603677, -0.9770955615653313941 ) ) ;
#18947=CARTESIAN_POINT ( 'NONE',  ( -16.94107738177414291, 14.24304960796391306, -219.3391119284832484 ) ) ;
#18968=EDGE_LOOP ( 'NONE', ( #46890, #65261, #70565, #102436 ) ) ;
#19431=CARTESIAN_POINT ( 'NONE',  ( -15.39946565075090845, 12.51008756600233873, -214.3176843001242560 ) ) ;
#19747=CIRCLE ( 'NONE', #202885, 14.30833333333333535 ) ;
#19849=AXIS2_PLACEMENT_3D ( 'NONE', #125427, #69310, #129273 ) ;
#19887=EDGE_CURVE ( 'NONE', #103723, #42401, #232505, .T. ) ;
#19952=CARTESIAN_POINT ( 'NONE',  ( -16.91256925476571027, 12.42391174447540081, -211.1203373714319014 ) ) ;
#20276=EDGE_CURVE ( 'NONE', #146298, #34114, #147556, .T. ) ;
#20282=AXIS2_PLACEMENT_3D ( 'NONE', #219121, #40546, #199603 ) ;
#20298=AXIS2_PLACEMENT_3D ( 'NONE', #241701, #223403, #203850 ) ;
#20425=PLANE ( 'NONE',  #160792 ) ;
#20450=CARTESIAN_POINT ( 'NONE',  ( -16.94389599338512298, 12.44527457180727836, -211.1927369019190621 ) ) ;
#20569=DIRECTION ( 'NONE',  ( -1.000000000000000000, 0.000000000000000000, 0.000000000000000000 ) ) ;
#20577=EDGE_LOOP ( 'NONE', ( #245375, #24396 ) ) ;
#20602=CARTESIAN_POINT ( 'NONE',  ( -16.84419801905645997, 14.15485412938328302, -219.2360291138972741 ) ) ;
#20676=CARTESIAN_POINT ( 'NONE',  ( -16.80621392010911208, 12.41483980993488245, -211.2832333842498826 ) ) ;
#20696=ORIENTED_EDGE ( 'NONE', *, *, #151468, .T. ) ;
#20733=LINE ( 'NONE', #100219, #239106 ) ;
#20877=CARTESIAN_POINT ( 'NONE',  ( -18.40000000000000213, 14.17280543801757986, -210.8598471598932349 ) ) ;
#20926=EDGE_CURVE ( 'NONE', #233793, #55301, #147037, .T. ) ;
#20981=MANIFOLD_SOLID_BREP ( 'Stock-MAS-200-1', #32659 ) ;
#21001=CARTESIAN_POINT ( 'NONE',  ( -16.97683810757273193, 14.02843185299666118, -218.6555494737106642 ) ) ;
#21196=LINE ( 'NONE', #1583, #9763 ) ;
#21257=CARTESIAN_POINT ( 'NONE',  ( -16.77683809663752257, 26.68086916408615750, -212.3318337774905160 ) ) ;
#21362=VERTEX_POINT ( 'NONE', #214356 ) ;
#21414=ORIENTED_EDGE ( 'NONE', *, *, #35413, .F. ) ;
#21558=VECTOR ( 'NONE', #123031, 1000.000000000000000 ) ;
#21617=CARTESIAN_POINT ( 'NONE',  ( -18.39999999999999858, 13.19494617735151465, -207.6708402378485516 ) ) ;
#21632=( BOUNDED_CURVE ( )  B_SPLINE_CURVE ( 3, ( #150677, #88097, #230204, #191106 ),
 .UNSPECIFIED., .F., .F. ) 
 B_SPLINE_CURVE_WITH_KNOTS ( ( 4, 4 ),
 ( -7.815970093361102045E-14, 1.570796326794882125 ),
 .UNSPECIFIED. ) 
 CURVE ( )  GEOMETRIC_REPRESENTATION_ITEM ( )  RATIONAL_B_SPLINE_CURVE ( ( 1.000000000000000000, 0.8047378541243499495, 0.8047378541243499495, 1.000000000000000000 ) ) 
 REPRESENTATION_ITEM ( '' )  );
#21682=AXIS2_PLACEMENT_3D ( 'NONE', #189534, #232526, #231238 ) ;
#21723=CARTESIAN_POINT ( 'NONE',  ( -16.92925196614875816, 12.42877699685184112, -211.2056432611043135 ) ) ;
#21968=CARTESIAN_POINT ( 'NONE',  ( -16.78055652883087134, 12.41318068003151431, -211.2541194833696068 ) ) ;
#21986=CARTESIAN_POINT ( 'NONE',  ( -17.11825945287482753, 12.51174298335651791, -211.2216088517780292 ) ) ;
#22052=ORIENTED_EDGE ( 'NONE', *, *, #220856, .F. ) ;
#22141=VECTOR ( 'NONE', #167526, 1000.000000000000000 ) ;
#22272=CARTESIAN_POINT ( 'NONE',  ( -16.87998658237740912, 14.11353887542160024, -219.0463262827253459 ) ) ;
#22408=CARTESIAN_POINT ( 'NONE',  ( -20.65000000000000568, 11.52084357182974195, -219.8296352432475942 ) ) ;
#22543=DIRECTION ( 'NONE',  ( 1.000000000000000000, 0.000000000000000000, 0.000000000000000000 ) ) ;
#22547=AXIS2_PLACEMENT_3D ( 'NONE', #101728, #126455, #143449 ) ;
#22752=MECHANICAL_DESIGN_GEOMETRIC_PRESENTATION_REPRESENTATION('',(#248145),#80968);
#22775=ADVANCED_FACE ( 'NONE', ( #109325 ), #28581, .T. ) ;
#22872=DIRECTION ( 'NONE',  ( 0.2834754621636358385, -0.4719347312574445619, 0.8348169091388102370 ) ) ;
#22917=ADVANCED_FACE ( 'NONE', ( #177046 ), #135307, .F. ) ;
#22978=VERTEX_POINT ( 'NONE', #40112 ) ;
#23213=CARTESIAN_POINT ( 'NONE',  ( -16.87036670365548474, 14.22508806334145959, -219.3732768077300932 ) ) ;
#23771=LINE ( 'NONE', #215811, #191559 ) ;
#23902=DIRECTION ( 'NONE',  ( -1.020425574104003999E-15, -0.2128009952263603677, 0.9770955615653313941 ) ) ;
#23988=CARTESIAN_POINT ( 'NONE',  ( 13.99999999999999822, 13.18880795147152618, -215.2702608532411830 ) ) ;
#24280=CARTESIAN_POINT ( 'NONE',  ( -16.87036670365548474, 14.22508806334146492, -219.3732768077300932 ) ) ;
#24326=CARTESIAN_POINT ( 'NONE',  ( -16.87036670365549895, 12.42497885867826390, -211.1079079717509046 ) ) ;
#24373=EDGE_LOOP ( 'NONE', ( #176205, #221795, #112777, #28502, #214268, #62990, #87756, #85945, #75121 ) ) ;
#24396=ORIENTED_EDGE ( 'NONE', *, *, #11514, .T. ) ;
#24553=AXIS2_PLACEMENT_3D ( 'NONE', #30175, #26309, #67991 ) ;
#24688=CYLINDRICAL_SURFACE ( 'NONE', #130131, 0.09999999999999939493 ) ;
#25005=CARTESIAN_POINT ( 'NONE',  ( -16.80100426158789872, 12.41435172007160403, -211.2765376762438052 ) ) ;
#25048=DIRECTION ( 'NONE',  ( -0.7071067811865462405, -0.6909108974501250167, -0.1504730267678050515 ) ) ;
#25366=DIRECTION ( 'NONE',  ( -1.073024830501117725E-15, -0.2128009952263603954, 0.9770955615653315052 ) ) ;
#25427=VERTEX_POINT ( 'NONE', #248591 ) ;
#25498=CARTESIAN_POINT ( 'NONE',  ( 13.99999999999999822, 13.18880795147152618, -215.2702608532411830 ) ) ;
#25536=CARTESIAN_POINT ( 'NONE',  ( -16.90137573187933029, 12.44348879280447129, -211.3781360020290379 ) ) ;
#25556=CARTESIAN_POINT ( 'NONE',  ( -17.80356949365270580, 15.56737101418502967, -221.3668113561435860 ) ) ;
#25645=DIRECTION ( 'NONE',  ( -0.000000000000000000, 0.2128009952263603677, -0.9770955615653313941 ) ) ;
#25753=CARTESIAN_POINT ( 'NONE',  ( -16.81453563122428108, 14.13521282870534357, -219.1970648546185885 ) ) ;
#25874=VECTOR ( 'NONE', #241832, 1000.000000000000000 ) ;
#25946=DIRECTION ( 'NONE',  ( -1.000000000000000000, 0.000000000000000000, 0.000000000000000000 ) ) ;
#26125=CARTESIAN_POINT ( 'NONE',  ( -16.87786941232800686, 14.17275468830522556, -219.2799003491669225 ) ) ;
#26309=DIRECTION ( 'NONE',  ( -1.000000000000000000, 0.000000000000000000, 0.000000000000000000 ) ) ;
#26327=PLANE ( 'NONE',  #19849 ) ;
#26425=CARTESIAN_POINT ( 'NONE',  ( -16.93935632781549572, 14.20137645198545862, -219.2864342127633961 ) ) ;
#26741=DIRECTION ( 'NONE',  ( 0.7071067811865388020, 0.6909108974501111389, 0.1504730267679034728 ) ) ;
#26745=CARTESIAN_POINT ( 'NONE',  ( 20.04999999999999716, 12.98648691417777101, -219.5104337504080263 ) ) ;
#26811=ADVANCED_FACE ( 'NONE', ( #72164 ), #170013, .F. ) ;
#26967=CARTESIAN_POINT ( 'NONE',  ( -16.94445028196807002, 14.20918193489391790, -219.2878138714100373 ) ) ;
#27067=CARTESIAN_POINT ( 'NONE',  ( -16.83794479845801462, 14.10322380767677863, -219.1100655228689220 ) ) ;
#27124=CARTESIAN_POINT ( 'NONE',  ( -16.81095280782811230, 12.41403342719979719, -211.2428889512998467 ) ) ;
#27140=CARTESIAN_POINT ( 'NONE',  ( -16.88005004766534967, 14.15917131436227372, -219.2553795824229610 ) ) ;
#27315=LINE ( 'NONE', #247603, #158045 ) ;
#27433=ADVANCED_FACE ( 'NONE', ( #92677 ), #194379, .T. ) ;
#27599=DIRECTION ( 'NONE',  ( 0.000000000000000000, 0.9770955615653315052, 0.2128009952263603954 ) ) ;
#27670=CIRCLE ( 'NONE', #69336, 0.9000000000000014655 ) ;
#27891=VECTOR ( 'NONE', #146590, 1000.000000000000227 ) ;
#27937=ORIENTED_EDGE ( 'NONE', *, *, #39212, .T. ) ;
#28502=ORIENTED_EDGE ( 'NONE', *, *, #51340, .F. ) ;
#28557=DIRECTION ( 'NONE',  ( 0.000000000000000000, 0.2128009952263603954, -0.9770955615653315052 ) ) ;
#28581=CYLINDRICAL_SURFACE ( 'NONE', #203648, 0.1999999999999987899 ) ;
#28593=CARTESIAN_POINT ( 'NONE',  ( -12.25000000000000178, 12.70026017068886404, -215.3766613508543628 ) ) ;
#28728=DIRECTION ( 'NONE',  ( -0.000000000000000000, 0.2128009952263603677, -0.9770955615653313941 ) ) ;
#28842=EDGE_CURVE ( 'NONE', #78646, #204749, #125757, .T. ) ;
#28915=EDGE_CURVE ( 'NONE', #223991, #180552, #42381, .T. ) ;
#29174=ORIENTED_EDGE ( 'NONE', *, *, #11859, .F. ) ;
#29324=ORIENTED_EDGE ( 'NONE', *, *, #72082, .T. ) ;
#29327=CARTESIAN_POINT ( 'NONE',  ( -15.55912972643741199, 10.96704414822730733, -211.4556836530944111 ) ) ;
#29785=DIRECTION ( 'NONE',  ( -1.000000000000000000, 1.614276770400120174E-15, 3.515722686956159758E-16 ) ) ;
#29805=CARTESIAN_POINT ( 'NONE',  ( -16.93658211146644987, 14.21365401117876814, -219.2987376607606507 ) ) ;
#29884=CARTESIAN_POINT ( 'NONE',  ( 18.39999999999999503, 10.68101405709484197, -223.4922417449319028 ) ) ;
#30036=ORIENTED_EDGE ( 'NONE', *, *, #20276, .T. ) ;
#30144=CARTESIAN_POINT ( 'NONE',  ( -16.88815647973233780, 12.41425476414399931, -211.2399925740093636 ) ) ;
#30175=CARTESIAN_POINT ( 'NONE',  ( -17.11825945287481332, 14.23543104469003673, -219.1360829004572395 ) ) ;
#30918=FACE_OUTER_BOUND ( 'NONE', #202081, .T. ) ;
#30990=CARTESIAN_POINT ( 'NONE',  ( -16.87665923198281348, 14.15900158805613884, -219.2550725561364118 ) ) ;
#31219=EDGE_CURVE ( 'NONE', #166393, #233837, #115901, .T. ) ;
#31279=ADVANCED_FACE ( 'NONE', ( #211344 ), #255542, .F. ) ;
#31396=DIRECTION ( 'NONE',  ( 1.000000000000000000, 0.000000000000000000, 0.000000000000000000 ) ) ;
#31457=ORIENTED_EDGE ( 'NONE', *, *, #213084, .F. ) ;
#31468=CARTESIAN_POINT ( 'NONE',  ( -23.25000000000000355, 14.17280543801757986, -210.8598471598932349 ) ) ;
#31791=ORIENTED_EDGE ( 'NONE', *, *, #98055, .T. ) ;
#31868=CARTESIAN_POINT ( 'NONE',  ( -18.40000000000000213, 8.212522512469059066, -212.1579332307740344 ) ) ;
#32148=DIRECTION ( 'NONE',  ( 0.000000000000000000, -0.9770955615653313941, -0.2128009952263603677 ) ) ;
#32190=PLANE ( 'NONE',  #214474 ) ;
#32206=CARTESIAN_POINT ( 'NONE',  ( 18.39999999999999503, 13.90230816252088530, -210.9187585823742666 ) ) ;
#32659=CLOSED_SHELL ( 'NONE', ( #62020, #5838, #131662, #27433, #249797, #5445, #11819, #68124, #227541, #137983, #179382, #214191, #223780, #254883, #206002, #53684, #65490, #132113, #253059, #70634, #39872, #236641, #118568, #31279, #226539, #22775, #221626, #14149, #120296, #60730, #22917, #116489, #156775, #353, #190736, #140390, #217402, #33417, #81335, #123610, #165362, #100554, #158569, #1955, #26811, #215907, #48390, #36232, #130134, #107997, #142180, #135197, #144598 ) ) ;
#32701=ORIENTED_EDGE ( 'NONE', *, *, #31219, .F. ) ;
#32744=DIRECTION ( 'NONE',  ( -0.000000000000000000, 0.2128009952263604232, -0.9770955615653316162 ) ) ;
#32792=VERTEX_POINT ( 'NONE', #17989 ) ;
#32959=CARTESIAN_POINT ( 'NONE',  ( -33.72168855820451938, 12.41403342719998903, -211.2428889513006425 ) ) ;
#33314=ORIENTED_EDGE ( 'NONE', *, *, #155967, .F. ) ;
#33417=ADVANCED_FACE ( 'NONE', ( #128357 ), #166223, .F. ) ;
#33420=( BOUNDED_SURFACE ( )  B_SPLINE_SURFACE ( 3, 2, ( 
 ( #2676, #142199, #1385 ),
 ( #97902, #57508, #21001 ),
 ( #178803, #221710, #61379 ),
 ( #121398, #241316, #43106 ),
 ( #120108, #22272, #159219 ),
 ( #238734, #18400, #160510 ),
 ( #139605, #100475, #58787 ),
 ( #177517, #108, #156667 ),
 ( #138322, #236164, #137066 ),
 ( #216600, #79638, #122659 ) ),
 .UNSPECIFIED., .F., .F., .F. ) 
 B_SPLINE_SURFACE_WITH_KNOTS ( ( 4, 2, 2, 2, 4 ),
 ( 3, 3 ),
 ( 0.002161241639767251272, 0.002579950749615826135, 0.002789305304540113349, 0.002893982582002256956, 0.002998659859464400564 ),
 ( 0.000000000000000000, 1.000000000000000000 ),
 .UNSPECIFIED. ) 
 GEOMETRIC_REPRESENTATION_ITEM ( )  RATIONAL_B_SPLINE_SURFACE ( (
 ( 1.000000000000000000, 0.7071067811865655584, 1.000000000000000000),
 ( 1.000000000000000000, 0.7632447400662427661, 1.000000000000000000),
 ( 1.000000000000000000, 0.8158073005112935761, 1.000000000000000000),
 ( 1.000000000000000000, 0.8906973462394487395, 1.000000000000000000),
 ( 1.000000000000000000, 0.9149408947805062198, 1.000000000000000000),
 ( 1.000000000000000000, 0.9493368785273317290, 1.000000000000000000),
 ( 1.000000000000000000, 0.9605194247157643472, 1.000000000000000000),
 ( 1.000000000000000000, 0.9803630264780097692, 1.000000000000000000),
 ( 1.000000000000000000, 0.9900844824271883837, 1.000000000000000000),
 ( 1.000000000000000000, 0.9894588281429257393, 1.000000000000000000) ) ) 
 REPRESENTATION_ITEM ( '' )  SURFACE ( )  );
#33493=DIRECTION ( 'NONE',  ( -1.020425574104003999E-15, 0.2128009952263603677, -0.9770955615653313941 ) ) ;
#33668=CARTESIAN_POINT ( 'NONE',  ( -16.93433913041102912, 14.23186370317824156, -219.3265704725438638 ) ) ;
#33708=CARTESIAN_POINT ( 'NONE',  ( 23.04999999999999716, 10.58889512527366428, -208.1606840254082158 ) ) ;
#33752=ORIENTED_EDGE ( 'NONE', *, *, #31219, .T. ) ;
#33848=ORIENTED_EDGE ( 'NONE', *, *, #170622, .F. ) ;
#33964=CARTESIAN_POINT ( 'NONE',  ( -14.00000000000000178, 13.18880795147152440, -215.2702608532411830 ) ) ;
#33999=EDGE_LOOP ( 'NONE', ( #78478, #174350, #90700, #118689 ) ) ;
#34114=VERTEX_POINT ( 'NONE', #83106 ) ;
#34772=ORIENTED_EDGE ( 'NONE', *, *, #82864, .T. ) ;
#35404=CYLINDRICAL_SURFACE ( 'NONE', #176699, 0.5000000000000004441 ) ;
#35413=EDGE_CURVE ( 'NONE', #209692, #103352, #94134, .T. ) ;
#35548=EDGE_CURVE ( 'NONE', #32792, #142560, #112090, .T. ) ;
#35607=VERTEX_POINT ( 'NONE', #92219 ) ;
#35796=PLANE ( 'NONE',  #108214 ) ;
#35942=VECTOR ( 'NONE', #165123, 1000.000000000000227 ) ;
#36108=CARTESIAN_POINT ( 'NONE',  ( 13.54556439290363379, 12.43810346549959611, -213.7002393734605619 ) ) ;
#36168=LINE ( 'NONE', #77828, #100302 ) ;
#36232=ADVANCED_FACE ( 'NONE', ( #145149 ), #184286, .T. ) ;
#36590=CARTESIAN_POINT ( 'NONE',  ( 14.88075390448863544, 13.10551310878183706, -216.8535402360471949 ) ) ;
#36729=DIRECTION ( 'NONE',  ( 1.000000000000000000, -1.156482317317869556E-14, 0.000000000000000000 ) ) ;
#36786=VECTOR ( 'NONE', #2357, 1000.000000000000227 ) ;
#36793=LINE ( 'NONE', #51147, #74321 ) ;
#36889=AXIS2_PLACEMENT_3D ( 'NONE', #102898, #200744, #179914 ) ;
#37030=CARTESIAN_POINT ( 'NONE',  ( -17.11825945287482043, 14.15900158805610509, -219.2550725561364402 ) ) ;
#37304=DIRECTION ( 'NONE',  ( 1.020425574104003999E-15, -0.2128009952263603677, 0.9770955615653313941 ) ) ;
#37395=CARTESIAN_POINT ( 'NONE',  ( 13.88302573338719093, 12.43282705614461925, -213.6439690125878883 ) ) ;
#37425=ORIENTED_EDGE ( 'NONE', *, *, #144413, .F. ) ;
#37458=ORIENTED_EDGE ( 'NONE', *, *, #183813, .T. ) ;
#37676=CARTESIAN_POINT ( 'NONE',  ( -16.80070461187888498, 12.41338732702360659, -211.2399223222487308 ) ) ;
#37731=CARTESIAN_POINT ( 'NONE',  ( -14.11697426661281440, 12.43282705614461747, -213.6439690125878315 ) ) ;
#37804=CARTESIAN_POINT ( 'NONE',  ( -12.25000000000000178, 13.18880795147152440, -215.2702608532411830 ) ) ;
#37833=CARTESIAN_POINT ( 'NONE',  ( -18.40000000000000213, 15.50909414388701890, -218.9610367925635330 ) ) ;
#37859=CARTESIAN_POINT ( 'NONE',  ( 12.60873083341396850, 12.96612044530440677, -216.4114274690425361 ) ) ;
#38228=CARTESIAN_POINT ( 'NONE',  ( -17.29158576265544056, 12.55694934947041119, -209.9501076257347734 ) ) ;
#38233=DIRECTION ( 'NONE',  ( -1.000000000000000000, 1.349229370204181174E-14, 0.000000000000000000 ) ) ;
#38300=CARTESIAN_POINT ( 'NONE',  ( -17.01764560440201990, 14.13772148870163647, -219.1573630007518432 ) ) ;
#38515=EDGE_LOOP ( 'NONE', ( #70347, #106593, #132638, #144758 ) ) ;
#38662=CARTESIAN_POINT ( 'NONE',  ( 12.93225390519045170, 12.47031117194349292, -214.0029172826438071 ) ) ;
#38760=ORIENTED_EDGE ( 'NONE', *, *, #213084, .T. ) ;
#38951=CARTESIAN_POINT ( 'NONE',  ( -16.77308656112214180, 12.41407453858650278, -211.2430777180555026 ) ) ;
#39065=CARTESIAN_POINT ( 'NONE',  ( 20.73486653747088582, 9.052352027204005225, -208.4953267290897259 ) ) ;
#39212=EDGE_CURVE ( 'NONE', #235384, #113827, #247879, .T. ) ;
#39310=CARTESIAN_POINT ( 'NONE',  ( -18.40000000000000213, 16.35463830854640932, -222.1788605317357224 ) ) ;
#39328=EDGE_CURVE ( 'NONE', #144652, #112987, #162202, .T. ) ;
#39331=CARTESIAN_POINT ( 'NONE',  ( -21.64999999999999858, 12.53302308287915245, -211.3193184079345883 ) ) ;
#39344=ORIENTED_EDGE ( 'NONE', *, *, #185519, .T. ) ;
#39589=DIRECTION ( 'NONE',  ( -0.000000000000000000, 0.2128009952263604232, -0.9770955615653316162 ) ) ;
#39836=CARTESIAN_POINT ( 'NONE',  ( 13.99999999999999822, 13.18880795147152618, -215.2702608532411830 ) ) ;
#39845=DIRECTION ( 'NONE',  ( -0.000000000000000000, 0.2128009952263603677, -0.9770955615653313941 ) ) ;
#39872=ADVANCED_FACE ( 'NONE', ( #223510 ), #117056, .F. ) ;
#40112=CARTESIAN_POINT ( 'NONE',  ( -18.40000000000000213, 15.66855642289968031, -219.0286517433665381 ) ) ;
#40288=CARTESIAN_POINT ( 'NONE',  ( -16.98495255085916611, 12.46505164876903216, -211.2160343393914559 ) ) ;
#40345=ORIENTED_EDGE ( 'NONE', *, *, #150216, .T. ) ;
#40546=DIRECTION ( 'NONE',  ( -1.073024830501117725E-15, 0.2128009952263604232, -0.9770955615653316162 ) ) ;
#40814=CARTESIAN_POINT ( 'NONE',  ( -16.92973740335338917, 12.44363429718260328, -211.1790690627998970 ) ) ;
#40819=DIRECTION ( 'NONE',  ( 1.000000000000000000, 1.159508501126949537E-16, 2.525285885220370376E-17 ) ) ;
#40855=ORIENTED_EDGE ( 'NONE', *, *, #181263, .T. ) ;
#41090=( BOUNDED_CURVE ( )  B_SPLINE_CURVE ( 3, ( #227263, #186882, #145147, #107315 ),
 .UNSPECIFIED., .F., .F. ) 
 B_SPLINE_CURVE_WITH_KNOTS ( ( 4, 4 ),
 ( 1.570796326794924536, 3.141592653589987183 ),
 .UNSPECIFIED. ) 
 CURVE ( )  GEOMETRIC_REPRESENTATION_ITEM ( )  RATIONAL_B_SPLINE_CURVE ( ( 1.000000000000000000, 0.8047378541243258576, 0.8047378541243258576, 1.000000000000000000 ) ) 
 REPRESENTATION_ITEM ( '' )  );
#41123=EDGE_LOOP ( 'NONE', ( #66344, #93412, #64226, #34772 ) ) ;
#41257=CARTESIAN_POINT ( 'NONE',  ( 14.45204356427542258, 12.43804190223350936, -213.6995959073539950 ) ) ;
#41409=ORIENTED_EDGE ( 'NONE', *, *, #204351, .T. ) ;
#41845=FACE_OUTER_BOUND ( 'NONE', #105744, .T. ) ;
#41934=CYLINDRICAL_SURFACE ( 'NONE', #154266, 0.9000000000000014655 ) ;
#41996=CARTESIAN_POINT ( 'NONE',  ( -16.85939591225058720, 12.43626824939381770, -211.5553831086668026 ) ) ;
#42008=CARTESIAN_POINT ( 'NONE',  ( -16.94445028196807002, 14.20918193489391790, -219.2878138714100373 ) ) ;
#42381=LINE ( 'NONE', #84020, #27891 ) ;
#42401=VERTEX_POINT ( 'NONE', #134854 ) ;
#42454=CARTESIAN_POINT ( 'NONE',  ( -16.92778301347381742, 14.22548837169992630, -219.3209511219291699 ) ) ;
#42489=EDGE_LOOP ( 'NONE', ( #224382, #234129, #239447 ) ) ;
#42634=DIRECTION ( 'NONE',  ( -1.652117596168391306E-15, -0.9770955615653313941, -0.2128009952263603677 ) ) ;
#42793=CARTESIAN_POINT ( 'NONE',  ( -20.65000000000000568, 11.52084357182974195, -219.8296352432475942 ) ) ;
#42857=CIRCLE ( 'NONE', #238487, 0.09999999999999810429 ) ;
#43054=ORIENTED_EDGE ( 'NONE', *, *, #73648, .F. ) ;
#43106=CARTESIAN_POINT ( 'NONE',  ( -16.93710578446435022, 14.10179983278268523, -218.9924253766343156 ) ) ;
#43207=EDGE_CURVE ( 'NONE', #146298, #234584, #74362, .T. ) ;
#43360=ORIENTED_EDGE ( 'NONE', *, *, #211617, .T. ) ;
#43403=LINE ( 'NONE', #239035, #148623 ) ;
#43468=AXIS2_PLACEMENT_3D ( 'NONE', #129003, #149859, #48162 ) ;
#43649=ORIENTED_EDGE ( 'NONE', *, *, #224337, .T. ) ;
#43929=CIRCLE ( 'NONE', #210530, 0.1999999999999987899 ) ;
#43987=CARTESIAN_POINT ( 'NONE',  ( 23.04999999999999716, 13.05738666989944363, -219.4949925395660557 ) ) ;
#44189=DIRECTION ( 'NONE',  ( -1.652117596168391306E-15, -0.9770955615653313941, -0.2128009952263603677 ) ) ;
#44420=CARTESIAN_POINT ( 'NONE',  ( -18.34374000495060386, 13.17878477875124688, -207.5966336730521391 ) ) ;
#44563=PLANE ( 'NONE',  #242716 ) ;
#44699=CARTESIAN_POINT ( 'NONE',  ( -16.94052228080551359, 14.20304230139262280, -219.2868029172807098 ) ) ;
#44889=ORIENTED_EDGE ( 'NONE', *, *, #15718, .T. ) ;
#44896=DIRECTION ( 'NONE',  ( -1.646408749285562691E-14, 0.9770955615653315052, 0.2128009952263603954 ) ) ;
#44911=FACE_OUTER_BOUND ( 'NONE', #12158, .T. ) ;
#45055=AXIS2_PLACEMENT_3D ( 'NONE', #100105, #80538, #61001 ) ;
#45086=CARTESIAN_POINT ( 'NONE',  ( -16.97683809663753252, 12.54629451653078043, -211.8501780441710309 ) ) ;
#45316=( LENGTH_UNIT ( ) NAMED_UNIT ( * ) SI_UNIT ( .MILLI., .METRE. ) );
#45533=CARTESIAN_POINT ( 'NONE',  ( -12.48127053791145791, 12.91284736048185344, -216.2278651779593304 ) ) ;
#45587=ORIENTED_EDGE ( 'NONE', *, *, #162436, .F. ) ;
#45635=ORIENTED_EDGE ( 'NONE', *, *, #234865, .F. ) ;
#45916=CARTESIAN_POINT ( 'NONE',  ( -16.89797118371785700, 12.42123379871372890, -211.1519811452710940 ) ) ;
#45973=CARTESIAN_POINT ( 'NONE',  ( 22.88900146558018989, 11.19647932930851120, -211.5080592518986862 ) ) ;
#46230=CARTESIAN_POINT ( 'NONE',  ( -16.87683809663752399, 23.44353604138475689, -208.8407808817581781 ) ) ;
#46327=( BOUNDED_SURFACE ( )  B_SPLINE_SURFACE ( 3, 2, ( 
 ( #129410, #249374, #107272 ),
 ( #130688, #227221, #85107 ),
 ( #86396, #66871, #126843 ),
 ( #166002, #69459, #47279 ) ),
 .UNSPECIFIED., .F., .F., .F. ) 
 B_SPLINE_SURFACE_WITH_KNOTS ( ( 4, 4 ),
 ( 3, 3 ),
 ( 4.712388980384689674, 5.765869716888459173 ),
 ( 0.000000000000000000, 1.000000000000000000 ),
 .UNSPECIFIED. ) 
 GEOMETRIC_REPRESENTATION_ITEM ( )  RATIONAL_B_SPLINE_SURFACE ( (
 ( 1.000000000000000000, 0.7071067811865795472, 1.000000000000000000),
 ( 1.000000000000000000, 0.7953136715913069477, 1.000000000000000000),
 ( 1.000000000000000000, 0.8646876308616193718, 1.000000000000000000),
 ( 1.000000000000000000, 0.8984936768950744224, 1.000000000000000000) ) ) 
 REPRESENTATION_ITEM ( '' )  SURFACE ( )  );
#46719=VERTEX_POINT ( 'NONE', #93307 ) ;
#46890=ORIENTED_EDGE ( 'NONE', *, *, #162904, .T. ) ;
#46932=LINE ( 'NONE', #228171, #91460 ) ;
#47254=ORIENTED_EDGE ( 'NONE', *, *, #71138, .F. ) ;
#47279=CARTESIAN_POINT ( 'NONE',  ( -16.93388492042258875, 12.44093641839707054, -211.1852997975874757 ) ) ;
#47526=LINE ( 'NONE', #52671, #167885 ) ;
#47566=ORIENTED_EDGE ( 'NONE', *, *, #97070, .F. ) ;
#47649=CARTESIAN_POINT ( 'NONE',  ( -17.73285935862227802, 15.55873092870509034, -221.4152481787321278 ) ) ;
#47801=ORIENTED_EDGE ( 'NONE', *, *, #169111, .T. ) ;
#47810=LINE ( 'NONE', #110366, #119691 ) ;
#48060=FACE_OUTER_BOUND ( 'NONE', #119101, .T. ) ;
#48162=DIRECTION ( 'NONE',  ( 1.000000000000000000, 1.159508501126949290E-16, 2.525285885220369759E-17 ) ) ;
#48237=ORIENTED_EDGE ( 'NONE', *, *, #231615, .T. ) ;
#48345=EDGE_CURVE ( 'NONE', #204749, #76812, #250510, .T. ) ;
#48359=CARTESIAN_POINT ( 'NONE',  ( -16.87845715379269507, 12.41613630788209655, -211.2156174692765376 ) ) ;
#48390=ADVANCED_FACE ( 'NONE', ( #198562 ), #133984, .T. ) ;
#48401=DIRECTION ( 'NONE',  ( -1.020425574104003999E-15, -0.2128009952263603677, 0.9770955615653313941 ) ) ;
#48540=CARTESIAN_POINT ( 'NONE',  ( 21.72449340488909897, 14.48530878454960735, -219.1840063279242088 ) ) ;
#48906=FILL_AREA_STYLE_COLOUR ( '', #214276 ) ;
#48928=CARTESIAN_POINT ( 'NONE',  ( -16.86132326855787156, 12.42438317058102193, -211.2904107606333071 ) ) ;
#49145=ORIENTED_EDGE ( 'NONE', *, *, #100524, .T. ) ;
#49326=LINE ( 'NONE', #22408, #107005 ) ;
#49340=CARTESIAN_POINT ( 'NONE',  ( -16.94107738177415712, 12.45552124806248706, -211.1315092113344463 ) ) ;
#49374=LINE ( 'NONE', #145888, #243193 ) ;
#49419=PLANE ( 'NONE',  #251751 ) ;
#49573=DIRECTION ( 'NONE',  ( 0.5932847527679296906, -0.7865547670005542669, -0.1713032417725948720 ) ) ;
#49919=EDGE_CURVE ( 'NONE', #21362, #187411, #68956, .T. ) ;
#50401=ORIENTED_EDGE ( 'NONE', *, *, #150216, .F. ) ;
#50527=EDGE_CURVE ( 'NONE', #76552, #183460, #23771, .T. ) ;
#50809=DIRECTION ( 'NONE',  ( 1.000000000000000000, 0.000000000000000000, 0.000000000000000000 ) ) ;
#50868=CARTESIAN_POINT ( 'NONE',  ( -23.25000000000000355, 15.91777359887373500, -218.8720307647289758 ) ) ;
#50900=CARTESIAN_POINT ( 'NONE',  ( -16.87036670365549895, 12.42497885867826390, -211.1079079717509046 ) ) ;
#51146=DIRECTION ( 'NONE',  ( 1.000000000000000000, 0.000000000000000000, 0.000000000000000000 ) ) ;
#51147=CARTESIAN_POINT ( 'NONE',  ( -16.77683809663752257, 14.15900158805613884, -219.2550725561364118 ) ) ;
#51340=EDGE_CURVE ( 'NONE', #88954, #205524, #199191, .T. ) ;
#51450=SURFACE_STYLE_FILL_AREA ( #88012 ) ;
#51582=CARTESIAN_POINT ( 'NONE',  ( -16.87036670365549895, 12.52461233780749872, -211.1164619086576408 ) ) ;
#51798=DIRECTION ( 'NONE',  ( -1.073024830501117725E-15, 0.2128009952263604232, -0.9770955615653316162 ) ) ;
#51896=DIRECTION ( 'NONE',  ( -3.035766082959430717E-14, 0.2128009952263604232, -0.9770955615653316162 ) ) ;
#51979=CARTESIAN_POINT ( 'NONE',  ( -17.27223548805715936, 12.52722179100237376, -209.9045420924107646 ) ) ;
#52671=CARTESIAN_POINT ( 'NONE',  ( 20.73486653747090003, 11.52084357182978458, -219.8296352432475658 ) ) ;
#52686=PLANE ( 'NONE',  #3791 ) ;
#52921=VECTOR ( 'NONE', #154401, 1000.000000000000000 ) ;
#52972=DIRECTION ( 'NONE',  ( -0.7071067811865486830, 0.6909108974501224631, 0.1504730267678053013 ) ) ;
#53249=EDGE_CURVE ( 'NONE', #186535, #3891, #100840, .T. ) ;
#53264=CARTESIAN_POINT ( 'NONE',  ( 18.39999999999999503, 13.90230816252088530, -210.9187585823742666 ) ) ;
#53494=DIRECTION ( 'NONE',  ( 1.186688945009009831E-16, -0.9770955615653313941, -0.2128009952263603677 ) ) ;
#53551=CARTESIAN_POINT ( 'NONE',  ( 20.99999999999999645, 11.49509093111729108, -207.9633242410238552 ) ) ;
#53684=ADVANCED_FACE ( 'NONE', ( #127536 ), #165385, .F. ) ;
#53727=B_SPLINE_CURVE_WITH_KNOTS ( 'NONE', 3,
 ( #221445, #256697, #119831, #1114, #19431, #201914, #157699, #158965, #136791, #76824, #59803, #216331, #37731, #156405, #218890, #199360, #80654, #160248, #239761, #203189, #126214, #67530, #127513, #63674, #244881, #147055 ),
 .UNSPECIFIED., .F., .F.,
 ( 4, 2, 2, 2, 2, 2, 2, 2, 2, 2, 2, 2, 4 ),
 ( 0.005476422646581355184, 0.006160811967703536639, 0.006845201288825718093, 0.007187395949386838311, 0.007529590609947957661, 0.007871785270509077878, 0.008213979931070198096, 0.008556174591631318313, 0.008898369252192438530, 0.009240563912753557013, 0.009582758573314677231, 0.01026714789443685868, 0.01095153721555904187 ),
 .UNSPECIFIED. ) ;
#54251=LINE ( 'NONE', #251159, #55848 ) ;
#54253=FACE_OUTER_BOUND ( 'NONE', #219809, .T. ) ;
#54312=PLANE ( 'NONE',  #59869 ) ;
#54372=CARTESIAN_POINT ( 'NONE',  ( 21.72449340488910607, 14.48530878454960202, -219.1840063279242088 ) ) ;
#54394=LINE ( 'NONE', #251300, #243183 ) ;
#54499=CARTESIAN_POINT ( 'NONE',  ( 18.39999999999999503, 8.212522512469059066, -212.1579332307740344 ) ) ;
#54636=CARTESIAN_POINT ( 'NONE',  ( -16.96982749440685012, 12.51506674510725858, -211.7067928272783490 ) ) ;
#55112=EDGE_CURVE ( 'NONE', #214748, #32792, #234706, .T. ) ;
#55191=CARTESIAN_POINT ( 'NONE',  ( -18.39418127959864790, 16.38129732710523001, -222.2507808268338465 ) ) ;
#55301=VERTEX_POINT ( 'NONE', #241141 ) ;
#55330=VERTEX_POINT ( 'NONE', #7651 ) ;
#55508=CARTESIAN_POINT ( 'NONE',  ( 16.27683809663750125, 11.10425270649115959, -208.0484446391143649 ) ) ;
#55616=CARTESIAN_POINT ( 'NONE',  ( 14.11444803880197085, 12.43281162335558676, -213.6438014222476056 ) ) ;
#55665=ORIENTED_EDGE ( 'NONE', *, *, #247727, .T. ) ;
#55697=CARTESIAN_POINT ( 'NONE',  ( -16.93521499325732549, 14.21491466131654668, -219.3013425272998518 ) ) ;
#55783=DIRECTION ( 'NONE',  ( 1.020425574104003999E-15, 0.2128009952263603677, -0.9770955615653313941 ) ) ;
#55848=VECTOR ( 'NONE', #154678, 1000.000000000000227 ) ;
#55900=CARTESIAN_POINT ( 'NONE',  ( -16.84793658983426567, 12.43183352348533610, -211.3246197489285976 ) ) ;
#56005=DIRECTION ( 'NONE',  ( -0.000000000000000000, 0.2128009952263603677, -0.9770955615653313941 ) ) ;
#56056=LINE ( 'NONE', #256790, #192318 ) ;
#56085=CARTESIAN_POINT ( 'NONE',  ( 15.69410316191959609, 12.80332707393613845, -215.8182015632437754 ) ) ;
#56232=ORIENTED_EDGE ( 'NONE', *, *, #229731, .T. ) ;
#56470=CARTESIAN_POINT ( 'NONE',  ( -16.94107738177415712, 12.45552124806248706, -211.1315092113344463 ) ) ;
#56680=DIRECTION ( 'NONE',  ( 0.000000000000000000, -0.2128009952263603954, 0.9770955615653315052 ) ) ;
#56845=CARTESIAN_POINT ( 'NONE',  ( -21.65000000000000213, 9.775875410973588586, -211.8174516384118817 ) ) ;
#56900=CARTESIAN_POINT ( 'NONE',  ( 14.77516762759920610, 12.45018385075468181, -213.8211107588515461 ) ) ;
#56993=CARTESIAN_POINT ( 'NONE',  ( 12.25000000000000000, 12.70026017068886937, -215.3766613508543628 ) ) ;
#57248=DIRECTION ( 'NONE',  ( 0.000000000000000000, 0.9770955615653313941, 0.2128009952263603677 ) ) ;
#57257=AXIS2_PLACEMENT_3D ( 'NONE', #162289, #44896, #222215 ) ;
#57508=CARTESIAN_POINT ( 'NONE',  ( -16.89155683852576217, 14.02549623409718471, -218.6420703064984821 ) ) ;
#57572=ORIENTED_EDGE ( 'NONE', *, *, #73307, .T. ) ;
#58093=ORIENTED_EDGE ( 'NONE', *, *, #181263, .F. ) ;
#58136=VERTEX_POINT ( 'NONE', #79694 ) ;
#58198=CARTESIAN_POINT ( 'NONE',  ( 14.22821877134046353, 12.43384112479209413, -213.6551227491177372 ) ) ;
#58257=ORIENTED_EDGE ( 'NONE', *, *, #222051, .T. ) ;
#58288=CARTESIAN_POINT ( 'NONE',  ( -16.87683809663752399, 13.90118822005493371, -218.5412211127979845 ) ) ;
#58511=CARTESIAN_POINT ( 'NONE',  ( 18.54999999999999716, 10.51799536955200232, -208.1761252362501864 ) ) ;
#58636=VECTOR ( 'NONE', #192864, 1000.000000000000227 ) ;
#58664=EDGE_CURVE ( 'NONE', #210119, #103572, #214671, .T. ) ;
#58787=CARTESIAN_POINT ( 'NONE',  ( -16.87401514999227103, 14.14410934721911239, -219.1866934472504624 ) ) ;
#58804=VERTEX_POINT ( 'NONE', #94469 ) ;
#58971=EDGE_CURVE ( 'NONE', #217875, #78646, #41090, .T. ) ;
#59110=CARTESIAN_POINT ( 'NONE',  ( -18.40000000000000213, 10.58889512527366428, -208.1606840254082158 ) ) ;
#59124=CARTESIAN_POINT ( 'NONE',  ( -16.79363873026997922, 14.15705967318782399, -219.2515591053820003 ) ) ;
#59283=DIRECTION ( 'NONE',  ( 0.000000000000000000, 0.2128009952263604232, -0.9770955615653316162 ) ) ;
#59362=DIRECTION ( 'NONE',  ( 0.000000000000000000, -0.8705263436746263350, -0.4921218192363414623 ) ) ;
#59496=DIRECTION ( 'NONE',  ( 0.000000000000000000, -0.9770955615653315052, -0.2128009952263603954 ) ) ;
#59501=EDGE_CURVE ( 'NONE', #35607, #155655, #258040, .T. ) ;
#59514=EDGE_CURVE ( 'NONE', #208323, #244309, #114733, .T. ) ;
#59750=CARTESIAN_POINT ( 'NONE',  ( -16.97683810757273193, 12.54460316225921446, -211.8424120337253385 ) ) ;
#59803=CARTESIAN_POINT ( 'NONE',  ( -14.45443560709636266, 12.43810346549959611, -213.7002393734605903 ) ) ;
#59869=AXIS2_PLACEMENT_3D ( 'NONE', #235519, #133861, #114298 ) ;
#60107=CARTESIAN_POINT ( 'NONE',  ( -16.93583594267724379, 12.45203240582405257, -211.1418800172411636 ) ) ;
#60125=CARTESIAN_POINT ( 'NONE',  ( 20.27550659511088682, 11.69688800608038193, -211.3990755776034405 ) ) ;
#60164=B_SPLINE_CURVE_WITH_KNOTS ( 'NONE', 3,
 ( #50900, #150057, #147464, #226997, #129195, #229580, #228297, #48359, #90045, #130464 ),
 .UNSPECIFIED., .F., .F.,
 ( 4, 3, 3, 4 ),
 ( 0.000000000000000000, 4.874959354402676393E-05, 9.785140065120904985E-05, 0.0001360444631936179696 ),
 .UNSPECIFIED. ) ;
#60226=DIRECTION ( 'NONE',  ( 0.000000000000000000, -0.9770955615653313941, -0.2128009952263603677 ) ) ;
#60324=EDGE_CURVE ( 'NONE', #17273, #240326, #162603, .T. ) ;
#60676=ORIENTED_EDGE ( 'NONE', *, *, #225405, .T. ) ;
#60728=ORIENTED_EDGE ( 'NONE', *, *, #98240, .T. ) ;
#60730=ADVANCED_FACE ( 'NONE', ( #200136 ), #64482, .F. ) ;
#60742=CYLINDRICAL_SURFACE ( 'NONE', #184977, 1.749999999999998002 ) ;
#60968=CARTESIAN_POINT ( 'NONE',  ( -14.00000000000000178, 13.18880795147152440, -215.2702608532411830 ) ) ;
#61001=DIRECTION ( 'NONE',  ( 1.000000000000000000, 0.000000000000000000, 0.000000000000000000 ) ) ;
#61073=CARTESIAN_POINT ( 'NONE',  ( -16.79184697841823848, 12.41370493160941635, -211.2471998651527656 ) ) ;
#61248=FACE_BOUND ( 'NONE', #9255, .T. ) ;
#61287=VECTOR ( 'NONE', #12775, 1000.000000000000000 ) ;
#61379=CARTESIAN_POINT ( 'NONE',  ( -16.96982749440682170, 14.05796827014931871, -218.7911686801608084 ) ) ;
#61528=CARTESIAN_POINT ( 'NONE',  ( 18.39999999999999147, 10.58889512527366428, -208.1606840254082158 ) ) ;
#61653=LINE ( 'NONE', #218136, #120870 ) ;
#61684=CARTESIAN_POINT ( 'NONE',  ( -16.92563707711777710, 14.18410270801246753, -219.2810851154148963 ) ) ;
#61842=EDGE_CURVE ( 'NONE', #212015, #169097, #140848, .T. ) ;
#61895=ORIENTED_EDGE ( 'NONE', *, *, #147259, .T. ) ;
#61946=DIRECTION ( 'NONE',  ( 1.000000000000000000, 0.000000000000000000, 0.000000000000000000 ) ) ;
#61949=CARTESIAN_POINT ( 'NONE',  ( -16.27683809663751191, 11.80649599073814215, -211.2728599922799617 ) ) ;
#62020=ADVANCED_FACE ( 'NONE', ( #244425 ), #145316, .F. ) ;
#62416=ORIENTED_EDGE ( 'NONE', *, *, #212572, .F. ) ;
#62680=CARTESIAN_POINT ( 'NONE',  ( -16.88460203013674743, 14.16703338188093575, -219.2695876520766092 ) ) ;
#62918=DIRECTION ( 'NONE',  ( 0.000000000000000000, 0.9770955615653317272, 0.2128009952263595073 ) ) ;
#62990=ORIENTED_EDGE ( 'NONE', *, *, #89203, .F. ) ;
#63073=DIRECTION ( 'NONE',  ( -1.000000000000000000, 0.000000000000000000, 0.000000000000000000 ) ) ;
#63237=EDGE_CURVE ( 'NONE', #169179, #155655, #47526, .T. ) ;
#63243=EDGE_CURVE ( 'NONE', #240326, #69452, #170114, .T. ) ;
#63297=CARTESIAN_POINT ( 'NONE',  ( -16.92570016628984320, 14.17383480627949410, -219.2818793572221523 ) ) ;
#63367=CARTESIAN_POINT ( 'NONE',  ( -17.78241384939014580, 15.55476280961775792, -221.4083347684370153 ) ) ;
#63403=VECTOR ( 'NONE', #23902, 1000.000000000000227 ) ;
#63438=DIRECTION ( 'NONE',  ( -0.000000000000000000, 0.2128009952263603677, -0.9770955615653313941 ) ) ;
#63674=CARTESIAN_POINT ( 'NONE',  ( -12.29659703204451660, 12.60783650272741241, -214.9246183040210667 ) ) ;
#63687=CARTESIAN_POINT ( 'NONE',  ( -33.72168855820452649, 16.37079970714665933, -222.2530670965321349 ) ) ;
#63833=VECTOR ( 'NONE', #226520, 1000.000000000000114 ) ;
#63956=DIRECTION ( 'NONE',  ( -0.5932847527679309119, 0.7865547670005533787, 0.1713032417725946777 ) ) ;
#63973=ORIENTED_EDGE ( 'NONE', *, *, #211617, .F. ) ;
#64027=CARTESIAN_POINT ( 'NONE',  ( -15.75000000000000355, 12.70026017068886937, -215.3766613508543628 ) ) ;
#64115=EDGE_CURVE ( 'NONE', #103572, #58136, #146096, .T. ) ;
#64226=ORIENTED_EDGE ( 'NONE', *, *, #120907, .F. ) ;
#64250=DIRECTION ( 'NONE',  ( -0.7071067811865456854, 0.6909108974501254608, 0.1504730267678059674 ) ) ;
#64269=ORIENTED_EDGE ( 'NONE', *, *, #162904, .F. ) ;
#64394=CARTESIAN_POINT ( 'NONE',  ( 20.05000000000002913, 9.052352027203996343, -208.4953267290897259 ) ) ;
#64482=PLANE ( 'NONE',  #209021 ) ;
#64525=CARTESIAN_POINT ( 'NONE',  ( 23.24999999999999645, 13.05738666989944363, -219.4949925395660557 ) ) ;
#64685=CARTESIAN_POINT ( 'NONE',  ( -16.94275863009466576, 12.44375159665070463, -211.1937418259165611 ) ) ;
#65069=EDGE_LOOP ( 'NONE', ( #44889, #169340, #213692, #181458, #11216, #115881 ) ) ;
#65171=ORIENTED_EDGE ( 'NONE', *, *, #224337, .F. ) ;
#65229=CARTESIAN_POINT ( 'NONE',  ( -16.86379686415369150, 14.20138720008526789, -219.3311860823795030 ) ) ;
#65261=ORIENTED_EDGE ( 'NONE', *, *, #178252, .T. ) ;
#65490=ADVANCED_FACE ( 'NONE', ( #234311 ), #20425, .F. ) ;
#65583=AXIS2_PLACEMENT_3D ( 'NONE', #194508, #94087, #36729 ) ;
#65644=ORIENTED_EDGE ( 'NONE', *, *, #39328, .T. ) ;
#65664=CARTESIAN_POINT ( 'NONE',  ( 16.87683809663749557, 14.15900158805613174, -219.2550725561364118 ) ) ;
#65835=FACE_OUTER_BOUND ( 'NONE', #239020, .T. ) ;
#66161=CARTESIAN_POINT ( 'NONE',  ( -17.71734398241074970, 15.53635165935942375, -221.3859150949375589 ) ) ;
#66162=SURFACE_SIDE_STYLE ('',( #223933 ) ) ;
#66195=LINE ( 'NONE', #162744, #63833 ) ;
#66344=ORIENTED_EDGE ( 'NONE', *, *, #239466, .T. ) ;
#66367=DIRECTION ( 'NONE',  ( 0.000000000000000000, 0.2128009952263603677, -0.9770955615653313941 ) ) ;
#66383=CARTESIAN_POINT ( 'NONE',  ( -12.68215100488890457, 12.99204546914880432, -216.4972940033653401 ) ) ;
#66490=LINE ( 'NONE', #146015, #58636 ) ;
#66871=CARTESIAN_POINT ( 'NONE',  ( -16.95709691156562471, 12.41617368651195541, -211.2527161509892153 ) ) ;
#66887=( BOUNDED_CURVE ( )  B_SPLINE_CURVE ( 3, ( #140328, #98604, #96064, #178216 ),
 .UNSPECIFIED., .F., .F. ) 
 B_SPLINE_CURVE_WITH_KNOTS ( ( 4, 4 ),
 ( 3.432212674861197854, 3.693332928900583401 ),
 .UNSPECIFIED. ) 
 CURVE ( )  GEOMETRIC_REPRESENTATION_ITEM ( )  RATIONAL_B_SPLINE_CURVE ( ( 1.000000000000000000, 0.9943260843901261525, 0.9943260843901261525, 1.000000000000000000 ) ) 
 REPRESENTATION_ITEM ( '' )  );
#66939=DIRECTION ( 'NONE',  ( 1.186688945009009831E-16, -0.9770955615653316162, -0.2128009952263604232 ) ) ;
#67089=DIRECTION ( 'NONE',  ( -1.186688945009009831E-16, 0.9770955615653313941, 0.2128009952263603677 ) ) ;
#67165=VECTOR ( 'NONE', #209818, 1000.000000000000227 ) ;
#67438=CARTESIAN_POINT ( 'NONE',  ( -16.81931177881022776, 14.12995618366871753, -219.1828163376052032 ) ) ;
#67526=DIRECTION ( 'NONE',  ( -1.000000000000000000, 1.614276770400120371E-15, 3.515722686956159758E-16 ) ) ;
#67530=CARTESIAN_POINT ( 'NONE',  ( -12.60206096961793065, 12.50981721680830105, -214.3157313002988644 ) ) ;
#67603=CARTESIAN_POINT ( 'NONE',  ( -18.40000000000000213, 8.212522512469059066, -212.1579332307740344 ) ) ;
#67660=CARTESIAN_POINT ( 'NONE',  ( -15.75000000000001066, 12.72457643131171245, -215.4883117230867526 ) ) ;
#67991=DIRECTION ( 'NONE',  ( 0.000000000000000000, -0.2128009952263403282, 0.9770955615653358350 ) ) ;
#68063=PRODUCT ( 'Snap Open Cable Crossbars 7', 'Snap Open Cable Crossbars 7', '', ( #215151 ) ) ;
#68124=ADVANCED_FACE ( 'NONE', ( #87553 ), #26327, .F. ) ;
#68480=ORIENTED_EDGE ( 'NONE', *, *, #19887, .T. ) ;
#68956=LINE ( 'NONE', #148476, #232685 ) ;
#69019=ORIENTED_EDGE ( 'NONE', *, *, #16129, .F. ) ;
#69226=FACE_OUTER_BOUND ( 'NONE', #242808, .T. ) ;
#69310=DIRECTION ( 'NONE',  ( 0.7071067811865493491, 0.6909108974501220191, 0.1504730267678052180 ) ) ;
#69336=AXIS2_PLACEMENT_3D ( 'NONE', #102690, #184815, #242219 ) ;
#69452=VERTEX_POINT ( 'NONE', #255621 ) ;
#69459=CARTESIAN_POINT ( 'NONE',  ( -16.91049119928365485, 12.40728329596000989, -211.2118950959028041 ) ) ;
#69925=DIRECTION ( 'NONE',  ( 0.2834754621636439431, -0.08203050052812088655, -0.9554646300801588055 ) ) ;
#70185=CARTESIAN_POINT ( 'NONE',  ( -21.64999999999999858, 11.10425270649115603, -208.0484446391143649 ) ) ;
#70200=CIRCLE ( 'NONE', #36889, 14.20833333333333748 ) ;
#70254=DIRECTION ( 'NONE',  ( -1.000000000000000000, 0.000000000000000000, 0.000000000000000000 ) ) ;
#70264=CARTESIAN_POINT ( 'NONE',  ( -13.54036565897076372, 13.16206247923560113, -217.0199023716218960 ) ) ;
#70347=ORIENTED_EDGE ( 'NONE', *, *, #208091, .T. ) ;
#70429=CARTESIAN_POINT ( 'NONE',  ( -18.35235881385853318, 13.17903599427090633, -207.5965789609904846 ) ) ;
#70565=ORIENTED_EDGE ( 'NONE', *, *, #239466, .F. ) ;
#70567=ORIENTED_EDGE ( 'NONE', *, *, #153924, .T. ) ;
#70634=ADVANCED_FACE ( 'NONE', ( #78661 ), #77375, .T. ) ;
#70701=EDGE_CURVE ( 'NONE', #96084, #200838, #218250, .T. ) ;
#70724=ORIENTED_EDGE ( 'NONE', *, *, #71165, .T. ) ;
#71029=CARTESIAN_POINT ( 'NONE',  ( 20.05000000000002913, 9.775875410973618784, -211.8174516384118817 ) ) ;
#71138=EDGE_CURVE ( 'NONE', #209692, #208323, #27670, .T. ) ;
#71165=EDGE_CURVE ( 'NONE', #220497, #101456, #91336, .T. ) ;
#71287=PLANE ( 'NONE',  #197041 ) ;
#71317=CARTESIAN_POINT ( 'NONE',  ( -16.27683809663751191, 11.10425270649114715, -208.0484446391143365 ) ) ;
#71433=DIRECTION ( 'NONE',  ( 0.000000000000000000, -0.2128009952263603677, 0.9770955615653313941 ) ) ;
#72082=EDGE_CURVE ( 'NONE', #244309, #103352, #189923, .T. ) ;
#72164=FACE_OUTER_BOUND ( 'NONE', #78849, .T. ) ;
#72678=CARTESIAN_POINT ( 'NONE',  ( 18.39999999999999503, 14.17280543801757986, -210.8598471598932349 ) ) ;
#72728=LINE ( 'NONE', #180790, #240563 ) ;
#72882=CARTESIAN_POINT ( 'NONE',  ( -16.91256925476571027, 12.42391174447540081, -211.1203373714319014 ) ) ;
#73093=DIRECTION ( 'NONE',  ( 0.000000000000000000, 0.2128009952263603677, -0.9770955615653313941 ) ) ;
#73110=DIRECTION ( 'NONE',  ( 1.000000000000000000, 0.000000000000000000, 0.000000000000000000 ) ) ;
#73147=CARTESIAN_POINT ( 'NONE',  ( 12.93279065517212523, 13.06253445771513100, -216.7219835687084526 ) ) ;
#73155=CARTESIAN_POINT ( 'NONE',  ( 23.04999999999999716, 10.58889512527366428, -208.1606840254082158 ) ) ;
#73174=ORIENTED_EDGE ( 'NONE', *, *, #70701, .T. ) ;
#73268=ORIENTED_EDGE ( 'NONE', *, *, #166495, .F. ) ;
#73307=EDGE_CURVE ( 'NONE', #171657, #217875, #100527, .T. ) ;
#73317=CARTESIAN_POINT ( 'NONE',  ( 15.74999999999999645, 12.70026017068886226, -215.3766613508543628 ) ) ;
#73552=EDGE_CURVE ( 'NONE', #76812, #82079, #74450, .T. ) ;
#73595=CARTESIAN_POINT ( 'NONE',  ( -16.91049119928363709, 14.16575171929611798, -219.2860664115342786 ) ) ;
#73648=EDGE_CURVE ( 'NONE', #101456, #187411, #221460, .T. ) ;
#73927=FACE_OUTER_BOUND ( 'NONE', #232671, .T. ) ;
#74183=DIRECTION ( 'NONE',  ( 1.000000000000000000, 0.000000000000000000, 0.000000000000000000 ) ) ;
#74250=CARTESIAN_POINT ( 'NONE',  ( -16.85722902420162228, 12.43862204461421150, -211.3557898750716788 ) ) ;
#74321=VECTOR ( 'NONE', #113720, 1000.000000000000000 ) ;
#74362=B_SPLINE_CURVE_WITH_KNOTS ( 'NONE', 3,
 ( #3415, #163804, #82935, #199070, #21723, #243316, #64685, #144207, #20450, #162531 ),
 .UNSPECIFIED., .F., .F.,
 ( 4, 3, 3, 4 ),
 ( 1.891508146150501351E-15, 3.877043166999833362E-05, 7.336897548476496527E-05, 7.659383120240286283E-05 ),
 .UNSPECIFIED. ) ;
#74404=DIRECTION ( 'NONE',  ( 1.186688945009009831E-16, -0.9770955615653313941, -0.2128009952263603677 ) ) ;
#74435=CARTESIAN_POINT ( 'NONE',  ( 12.42718393586865844, 12.88553809045802723, -216.1303193953968673 ) ) ;
#74450=B_SPLINE_CURVE_WITH_KNOTS ( 'NONE', 3,
 ( #134234, #196777, #78113, #234633 ),
 .UNSPECIFIED., .F., .F.,
 ( 4, 4 ),
 ( 0.000000000000000000, 7.713889350928925437E-05 ),
 .UNSPECIFIED. ) ;
#74758=AXIS2_PLACEMENT_3D ( 'NONE', #21257, #40819, #62918 ) ;
#74792=CIRCLE ( 'NONE', #145635, 0.1000000000000006301 ) ;
#74931=FACE_OUTER_BOUND ( 'NONE', #174638, .T. ) ;
#75121=ORIENTED_EDGE ( 'NONE', *, *, #185519, .F. ) ;
#75285=ORIENTED_EDGE ( 'NONE', *, *, #157663, .F. ) ;
#75340=CARTESIAN_POINT ( 'NONE',  ( -16.93211319090181632, 14.22327269246674852, -219.3152801208867118 ) ) ;
#75520=CARTESIAN_POINT ( 'NONE',  ( -16.87998658237730965, 12.45949613983442994, -211.4516352247128168 ) ) ;
#75555=EDGE_CURVE ( 'NONE', #34114, #103572, #61653, .T. ) ;
#75631=DIRECTION ( 'NONE',  ( 1.000000000000000000, 0.000000000000000000, 0.000000000000000000 ) ) ;
#75703=DIRECTION ( 'NONE',  ( 0.000000000000000000, -0.2128009952263603954, 0.9770955615653315052 ) ) ;
#75897=ORIENTED_EDGE ( 'NONE', *, *, #93725, .F. ) ;
#76042=CARTESIAN_POINT ( 'NONE',  ( 16.87683809663750267, 12.41403342719998371, -211.2428889513006993 ) ) ;
#76129=EDGE_CURVE ( 'NONE', #212015, #22978, #66490, .T. ) ;
#76269=FACE_OUTER_BOUND ( 'NONE', #24373, .T. ) ;
#76552=VERTEX_POINT ( 'NONE', #32206 ) ;
#76812=VERTEX_POINT ( 'NONE', #21617 ) ;
#76824=CARTESIAN_POINT ( 'NONE',  ( -14.56556274378147542, 12.44134409367007521, -213.7340784654984986 ) ) ;
#77116=CARTESIAN_POINT ( 'NONE',  ( -16.93262454970420094, 12.44846049787371278, -211.1565081053942663 ) ) ;
#77129=ORIENTED_EDGE ( 'NONE', *, *, #103318, .F. ) ;
#77375=CYLINDRICAL_SURFACE ( 'NONE', #6595, 1.500000000000001332 ) ;
#77762=CARTESIAN_POINT ( 'NONE',  ( 15.75000000000000000, 12.65101141449787292, -215.1505311063240526 ) ) ;
#77767=VECTOR ( 'NONE', #226673, 1000.000000000000227 ) ;
#77794=EDGE_CURVE ( 'NONE', #167344, #183460, #153053, .T. ) ;
#77828=CARTESIAN_POINT ( 'NONE',  ( 18.39999999999999503, 14.17280543801757986, -210.8598471598932349 ) ) ;
#77952=ORIENTED_EDGE ( 'NONE', *, *, #99074, .F. ) ;
#78113=CARTESIAN_POINT ( 'NONE',  ( -18.39999999999999858, 13.18942546263217785, -207.6195883042091737 ) ) ;
#78224=ORIENTED_EDGE ( 'NONE', *, *, #127764, .F. ) ;
#78412=ORIENTED_EDGE ( 'NONE', *, *, #221212, .T. ) ;
#78419=EDGE_CURVE ( 'NONE', #46719, #183460, #12093, .T. ) ;
#78429=VECTOR ( 'NONE', #121076, 1000.000000000000000 ) ;
#78478=ORIENTED_EDGE ( 'NONE', *, *, #121053, .F. ) ;
#78646=VERTEX_POINT ( 'NONE', #87433 ) ;
#78661=FACE_OUTER_BOUND ( 'NONE', #114009, .T. ) ;
#78701=CARTESIAN_POINT ( 'NONE',  ( -16.77779411440718249, 14.15241369799481674, -219.2431438278712221 ) ) ;
#78728=ORIENTED_EDGE ( 'NONE', *, *, #59514, .F. ) ;
#78849=EDGE_LOOP ( 'NONE', ( #103945, #146080, #220368, #243241, #158072 ) ) ;
#79536=ORIENTED_EDGE ( 'NONE', *, *, #227729, .T. ) ;
#79638=CARTESIAN_POINT ( 'NONE',  ( -16.77308656112213470, 14.15896047666961977, -219.2548837893815801 ) ) ;
#79694=CARTESIAN_POINT ( 'NONE',  ( -16.77683809663752257, 12.41293291551535916, -211.2574046339461233 ) ) ;
#79858=( BOUNDED_CURVE ( )  B_SPLINE_CURVE ( 3, ( #21986, #101454, #40288, #138047 ),
 .UNSPECIFIED., .F., .F. ) 
 B_SPLINE_CURVE_WITH_KNOTS ( ( 4, 4 ),
 ( 4.712388980384689674, 5.672655318024873772 ),
 .UNSPECIFIED. ) 
 CURVE ( )  GEOMETRIC_REPRESENTATION_ITEM ( )  RATIONAL_B_SPLINE_CURVE ( ( 1.000000000000000000, 0.9246222802177073152, 0.9246222802177073152, 1.000000000000000000 ) ) 
 REPRESENTATION_ITEM ( '' )  );
#80217=VECTOR ( 'NONE', #187271, 1000.000000000000227 ) ;
#80515=CARTESIAN_POINT ( 'NONE',  ( -16.97683809663752186, 13.99889777621145903, -218.5199410132753144 ) ) ;
#80538=DIRECTION ( 'NONE',  ( 1.186688945009010077E-16, -0.9770955615653316162, -0.2128009952263604232 ) ) ;
#80654=CARTESIAN_POINT ( 'NONE',  ( -13.43673303185028978, 12.44126776692609759, -213.7332981774226539 ) ) ;
#80705=EDGE_LOOP ( 'NONE', ( #94166, #254730, #141668, #78224 ) ) ;
#80801=B_SPLINE_CURVE_WITH_KNOTS ( 'NONE', 3,
 ( #233640, #99227, #17169, #118834, #134, #18430, #159245, #176245, #15895, #154137, #255710, #238766, #77116, #156693, #60107, #97935, #135793, #236188, #219185 ),
 .UNSPECIFIED., .F., .F.,
 ( 4, 3, 3, 3, 3, 3, 4 ),
 ( 0.0001624081864585780774, 0.0001685232196531779832, 0.0001764526673566780949, 0.0001916878551483017082, 0.0002009890782182522653, 0.0002238845907554767498, 0.0002283406619926077572 ),
 .UNSPECIFIED. ) ;
#80968=( GEOMETRIC_REPRESENTATION_CONTEXT ( 3 ) GLOBAL_UNCERTAINTY_ASSIGNED_CONTEXT ( ( #212038 ) ) GLOBAL_UNIT_ASSIGNED_CONTEXT ( ( #230116, #9783, #131015 ) ) REPRESENTATION_CONTEXT ( 'NONE', 'WORKASPACE' ) );
#81006=B_SPLINE_CURVE_WITH_KNOTS ( 'NONE', 3,
 ( #88331, #150905, #190037, #13975 ),
 .UNSPECIFIED., .F., .F.,
 ( 4, 4 ),
 ( 0.000000000000000000, 7.713889350930496175E-05 ),
 .UNSPECIFIED. ) ;
#81264=EDGE_CURVE ( 'NONE', #202859, #119125, #120256, .T. ) ;
#81335=ADVANCED_FACE ( 'NONE', ( #109335 ), #10271, .T. ) ;
#81383=ORIENTED_EDGE ( 'NONE', *, *, #207699, .F. ) ;
#81553=CARTESIAN_POINT ( 'NONE',  ( -16.89797118371758344, 14.20335419055749604, -219.3347526740980129 ) ) ;
#81848=EDGE_CURVE ( 'NONE', #112987, #204749, #74792, .T. ) ;
#82015=CARTESIAN_POINT ( 'NONE',  ( 20.73486653747088582, 11.52084357182978458, -219.8296352432475658 ) ) ;
#82056=PRODUCT_DEFINITION_FORMATION_WITH_SPECIFIED_SOURCE ( 'ANY', '', #68063, .NOT_KNOWN. ) ;
#82058=CARTESIAN_POINT ( 'NONE',  ( -33.72168855820452649, 26.68086916408615750, -212.3318337774905160 ) ) ;
#82079=VERTEX_POINT ( 'NONE', #205240 ) ;
#82328=AXIS2_PLACEMENT_3D ( 'NONE', #203970, #25366, #184404 ) ;
#82347=CARTESIAN_POINT ( 'NONE',  ( -16.81930730667006912, 12.41766554746485518, -211.3206651839645360 ) ) ;
#82832=CARTESIAN_POINT ( 'NONE',  ( -16.89318236219976299, 14.16159327252907651, -219.2597579924957358 ) ) ;
#82864=EDGE_CURVE ( 'NONE', #104329, #17273, #184735, .T. ) ;
#82935=CARTESIAN_POINT ( 'NONE',  ( -16.91247567987037570, 12.41838062070308624, -211.2201679100434717 ) ) ;
#82986=CARTESIAN_POINT ( 'NONE',  ( -16.87683809663752399, 12.31632387104345305, -211.2641690508233125 ) ) ;
#83070=DIRECTION ( 'NONE',  ( 1.000000000000000000, 0.000000000000000000, 0.000000000000000000 ) ) ;
#83106=CARTESIAN_POINT ( 'NONE',  ( -16.87331047859651179, 12.41403342719998726, -211.2428889513006993 ) ) ;
#83214=ORIENTED_EDGE ( 'NONE', *, *, #81848, .T. ) ;
#83307=EDGE_LOOP ( 'NONE', ( #135256, #177539, #185307, #214232, #120011, #224293, #47254, #188042, #33314, #121107, #99037, #200558, #143421, #175825 ) ) ;
#83626=CARTESIAN_POINT ( 'NONE',  ( -16.80468759584936933, 12.41488287255450373, -211.2836609135854928 ) ) ;
#83763=ORIENTED_EDGE ( 'NONE', *, *, #236304, .T. ) ;
#83824=CARTESIAN_POINT ( 'NONE',  ( -18.40000000000000213, 13.76412598303084778, -210.9488531877278206 ) ) ;
#83839=VECTOR ( 'NONE', #113813, 1000.000000000000227 ) ;
#83934=APPLICATION_CONTEXT ( 'automotive_design' ) ;
#84020=CARTESIAN_POINT ( 'NONE',  ( 22.88900146558018989, 10.47295594553888343, -208.1859343425765303 ) ) ;
#84099=ORIENTED_EDGE ( 'NONE', *, *, #193394, .T. ) ;
#84114=AXIS2_PLACEMENT_3D ( 'NONE', #246541, #31396, #73093 ) ;
#84241=CARTESIAN_POINT ( 'NONE',  ( 20.73486653747088226, 9.775875410973629442, -211.8174516384118533 ) ) ;
#84292=VECTOR ( 'NONE', #63438, 1000.000000000000227 ) ;
#84402=ORIENTED_EDGE ( 'NONE', *, *, #99074, .T. ) ;
#84915=CARTESIAN_POINT ( 'NONE',  ( -16.79139129368503802, 12.41340146879463724, -211.2637457794402280 ) ) ;
#84962=VERTEX_POINT ( 'NONE', #89759 ) ;
#85012=CARTESIAN_POINT ( 'NONE',  ( -16.92570016628985030, 12.41637551217347379, -211.2123415523068104 ) ) ;
#85107=CARTESIAN_POINT ( 'NONE',  ( -17.04295772865421910, 12.48721732318495548, -211.2269502790635727 ) ) ;
#85541=LINE ( 'NONE', #206816, #35942 ) ;
#85891=CARTESIAN_POINT ( 'NONE',  ( -16.87331047859649757, 14.15900158805613884, -219.2550725561364118 ) ) ;
#85945=ORIENTED_EDGE ( 'NONE', *, *, #234865, .T. ) ;
#86007=EDGE_LOOP ( 'NONE', ( #37425, #124456, #238018, #228084 ) ) ;
#86346=CARTESIAN_POINT ( 'NONE',  ( -16.93301857435213975, 14.19232141894375410, -219.2844300510592177 ) ) ;
#86396=CARTESIAN_POINT ( 'NONE',  ( -16.92209698673947571, 12.42693673621513994, -211.3021356947419349 ) ) ;
#86529=ORIENTED_EDGE ( 'NONE', *, *, #104637, .F. ) ;
#86774=EDGE_CURVE ( 'NONE', #25427, #35607, #193089, .T. ) ;
#87433=CARTESIAN_POINT ( 'NONE',  ( -18.40000000000000213, 13.88102806299823833, -210.8210490262177359 ) ) ;
#87553=FACE_OUTER_BOUND ( 'NONE', #107555, .T. ) ;
#87756=ORIENTED_EDGE ( 'NONE', *, *, #143802, .T. ) ;
#88012=FILL_AREA_STYLE ('',( #48906 ) ) ;
#88071=ORIENTED_EDGE ( 'NONE', *, *, #231947, .T. ) ;
#88097=CARTESIAN_POINT ( 'NONE',  ( -18.40000000000000213, 15.65609082920797412, -218.9714148105434788 ) ) ;
#88320=ORIENTED_EDGE ( 'NONE', *, *, #12892, .T. ) ;
#88326=CARTESIAN_POINT ( 'NONE',  ( -16.89268316805465986, 14.16190809729244648, -219.2603268738197073 ) ) ;
#88331=CARTESIAN_POINT ( 'NONE',  ( -18.40000000000000213, 16.38400329561159907, -222.2501914957450424 ) ) ;
#88481=CARTESIAN_POINT ( 'NONE',  ( -14.77538296656415007, 13.11968191886198376, -216.8952266020228308 ) ) ;
#88533=CARTESIAN_POINT ( 'NONE',  ( -18.37013991200266005, 13.19560622132187078, -207.5489386142775174 ) ) ;
#88542=B_SPLINE_CURVE_WITH_KNOTS ( 'NONE', 3,
 ( #254666, #93062, #232611, #175226, #172663, #55191, #211749 ),
 .UNSPECIFIED., .F., .F.,
 ( 4, 3, 4 ),
 ( 0.000000000000000000, 3.882884552234292441E-05, 5.798605692158292918E-05 ),
 .UNSPECIFIED. ) ;
#88543=ORIENTED_EDGE ( 'NONE', *, *, #76129, .F. ) ;
#88557=CARTESIAN_POINT ( 'NONE',  ( -18.40000000000000213, 13.78091005366907140, -222.8171174488881832 ) ) ;
#88559=FACE_OUTER_BOUND ( 'NONE', #20577, .T. ) ;
#88814=AXIS2_PLACEMENT_3D ( 'NONE', #230462, #51798, #252577 ) ;
#88952=CARTESIAN_POINT ( 'NONE',  ( -16.87036670365548474, 14.22508806334145959, -219.3732768077300932 ) ) ;
#88954=VERTEX_POINT ( 'NONE', #42793 ) ;
#89001=CARTESIAN_POINT ( 'NONE',  ( -23.25000000000000355, 7.488999128699433072, -208.8358083214519070 ) ) ;
#89203=EDGE_CURVE ( 'NONE', #251152, #84962, #49374, .T. ) ;
#89561=CARTESIAN_POINT ( 'NONE',  ( -16.80100914604133067, 14.14529455580030515, -219.2243293987745858 ) ) ;
#89579=ORIENTED_EDGE ( 'NONE', *, *, #53249, .T. ) ;
#89652=ORIENTED_EDGE ( 'NONE', *, *, #97280, .T. ) ;
#89759=CARTESIAN_POINT ( 'NONE',  ( -20.65000000000000568, 9.957490673325212427, -220.1701168356097469 ) ) ;
#89779=CARTESIAN_POINT ( 'NONE',  ( -23.25000000000000355, 11.69051004343035771, -207.9207640419785719 ) ) ;
#89938=CARTESIAN_POINT ( 'NONE',  ( -18.35663730107557257, 13.17951322611091491, -207.5964750249841302 ) ) ;
#90045=CARTESIAN_POINT ( 'NONE',  ( -16.88495309932520883, 12.41526644790654288, -211.2268068864140105 ) ) ;
#90078=CARTESIAN_POINT ( 'NONE',  ( -16.88560720703333473, 12.41418354840153526, -211.2409239182446470 ) ) ;
#90091=ORIENTED_EDGE ( 'NONE', *, *, #184433, .T. ) ;
#90409=PLANE ( 'NONE',  #21682 ) ;
#90420=CARTESIAN_POINT ( 'NONE',  ( -20.65000000000000568, 9.052352027203962592, -208.4953267290897543 ) ) ;
#90488=VECTOR ( 'NONE', #126548, 1000.000000000000000 ) ;
#90700=ORIENTED_EDGE ( 'NONE', *, *, #143868, .F. ) ;
#90799=ORIENTED_EDGE ( 'NONE', *, *, #81264, .F. ) ;
#90897=VECTOR ( 'NONE', #131613, 1000.000000000000227 ) ;
#90962=VECTOR ( 'NONE', #239747, 1000.000000000000227 ) ;
#91046=LINE ( 'NONE', #132761, #1397 ) ;
#91052=( GEOMETRIC_REPRESENTATION_CONTEXT ( 3 ) GLOBAL_UNCERTAINTY_ASSIGNED_CONTEXT ( ( #158863 ) ) GLOBAL_UNIT_ASSIGNED_CONTEXT ( ( #45316, #247355, #149575 ) ) REPRESENTATION_CONTEXT ( 'NONE', 'WORKASPACE' ) );
#91336=( BOUNDED_CURVE ( )  B_SPLINE_CURVE ( 3, ( #23213, #226490, #66161, #106547 ),
 .UNSPECIFIED., .F., .F. ) 
 B_SPLINE_CURVE_WITH_KNOTS ( ( 4, 4 ),
 ( 0.3000847527772391721, 0.5517402753107903957 ),
 .UNSPECIFIED. ) 
 CURVE ( )  GEOMETRIC_REPRESENTATION_ITEM ( )  RATIONAL_B_SPLINE_CURVE ( ( 1.000000000000000000, 0.9947294176030464508, 0.9947294176030464508, 1.000000000000000000 ) ) 
 REPRESENTATION_ITEM ( '' )  );
#91388=VERTEX_POINT ( 'NONE', #156918 ) ;
#91460=VECTOR ( 'NONE', #28728, 1000.000000000000227 ) ;
#91683=EDGE_LOOP ( 'NONE', ( #148200, #138754, #216053, #165967 ) ) ;
#91936=EDGE_LOOP ( 'NONE', ( #173928, #84402, #159061, #146205, #61895, #194784, #140335, #202772, #13483, #256124 ) ) ;
#92082=B_SPLINE_CURVE_WITH_KNOTS ( 'NONE', 3,
 ( #234279, #175619, #235562, #136447, #176913, #215993, #38662, #195196, #178196, #219853, #36108, #16545, #37395, #55616, #58198, #41257, #256354, #56900, #97309, #193897, #214722, #196438, #17794, #137737, #77762, #118197 ),
 .UNSPECIFIED., .F., .F.,
 ( 4, 2, 2, 2, 2, 2, 2, 2, 2, 2, 2, 2, 4 ),
 ( 0.005476422646581346511, 0.006160811967703526230, 0.006845201288825705950, 0.007187395949386825300, 0.007529590609947943783, 0.007871785270509062266, 0.008213979931070182483, 0.008556174591631300966, 0.008898369252192419449, 0.009240563912753537931, 0.009582758573314656414, 0.01026714789443684134, 0.01095153721555902279 ),
 .UNSPECIFIED. ) ;
#92186=CARTESIAN_POINT ( 'NONE',  ( -16.77732147278574715, 12.41296741182544849, -211.2569465384485170 ) ) ;
#92217=ORIENTED_EDGE ( 'NONE', *, *, #247251, .F. ) ;
#92219=CARTESIAN_POINT ( 'NONE',  ( 20.73486653747088582, 9.775875410973629442, -211.8174516384118533 ) ) ;
#92668=CARTESIAN_POINT ( 'NONE',  ( 15.51872946208856696, 12.91284736048184634, -216.2278651779593304 ) ) ;
#92677=FACE_OUTER_BOUND ( 'NONE', #104656, .T. ) ;
#92754=ORIENTED_EDGE ( 'NONE', *, *, #75555, .T. ) ;
#92755=CARTESIAN_POINT ( 'NONE',  ( 20.73486653747088937, 9.540899807986670922, -208.3889262314765460 ) ) ;
#93062=CARTESIAN_POINT ( 'NONE',  ( -18.35668295345803713, 16.37079970714665933, -222.2530670965321349 ) ) ;
#93111=CIRCLE ( 'NONE', #201257, 0.9000000000000014655 ) ;
#93165=EDGE_CURVE ( 'NONE', #175353, #220350, #72728, .T. ) ;
#93307=CARTESIAN_POINT ( 'NONE',  ( 18.54999999999999716, 12.41403342719998548, -211.2428889513006425 ) ) ;
#93412=ORIENTED_EDGE ( 'NONE', *, *, #51340, .T. ) ;
#93704=DIRECTION ( 'NONE',  ( 1.186688945009009831E-16, -0.9770955615653316162, -0.2128009952263604232 ) ) ;
#93725=EDGE_CURVE ( 'NONE', #135298, #94156, #7503, .T. ) ;
#93931=CARTESIAN_POINT ( 'NONE',  ( -16.87036670365548474, 14.22508806334145959, -219.3732768077300932 ) ) ;
#93952=CARTESIAN_POINT ( 'NONE',  ( 13.54577453029515510, 13.15902077901803402, -217.0103513519799776 ) ) ;
#94087=DIRECTION ( 'NONE',  ( 1.073024830501117725E-15, 0.2128009952263604232, -0.9770955615653316162 ) ) ;
#94134=LINE ( 'NONE', #95426, #203824 ) ;
#94156=VERTEX_POINT ( 'NONE', #130461 ) ;
#94166=ORIENTED_EDGE ( 'NONE', *, *, #196340, .T. ) ;
#94451=AXIS2_PLACEMENT_3D ( 'NONE', #11733, #225592, #50809 ) ;
#94455=DIRECTION ( 'NONE',  ( -0.8049926720990042694, -0.5796958986739304542, -0.1262515858416409231 ) ) ;
#94469=CARTESIAN_POINT ( 'NONE',  ( -16.87683809663752399, 12.47642768288813286, -211.9993005936843815 ) ) ;
#94716=CARTESIAN_POINT ( 'NONE',  ( 18.54999999999999716, 10.51799536955200232, -208.1761252362501864 ) ) ;
#94887=CARTESIAN_POINT ( 'NONE',  ( -16.97683809663752186, 12.47642768288816661, -211.9993005936845805 ) ) ;
#95052=CARTESIAN_POINT ( 'NONE',  ( -16.97683809663752186, 12.57413723904469904, -211.9780204941619388 ) ) ;
#95238=CARTESIAN_POINT ( 'NONE',  ( 15.31784899511109721, 12.99204546914880254, -216.4972940033653401 ) ) ;
#95283=ORIENTED_EDGE ( 'NONE', *, *, #151468, .F. ) ;
#95381=ORIENTED_EDGE ( 'NONE', *, *, #212572, .T. ) ;
#95426=CARTESIAN_POINT ( 'NONE',  ( 20.09999999999999787, 11.49509093111729108, -207.9633242410238552 ) ) ;
#95779=( BOUNDED_CURVE ( )  B_SPLINE_CURVE ( 3, ( #42008, #165810, #225732, #2838 ),
 .UNSPECIFIED., .F., .F. ) 
 B_SPLINE_CURVE_WITH_KNOTS ( ( 4, 4 ),
 ( 3.752122642744651682, 4.712388980384675463 ),
 .UNSPECIFIED. ) 
 CURVE ( )  GEOMETRIC_REPRESENTATION_ITEM ( )  RATIONAL_B_SPLINE_CURVE ( ( 1.000000000000000000, 0.9246222802177319622, 0.9246222802177319622, 1.000000000000000000 ) ) 
 REPRESENTATION_ITEM ( '' )  );
#96064=CARTESIAN_POINT ( 'NONE',  ( 17.74533788810830970, 15.50479229951815263, -221.3531188506081548 ) ) ;
#96084=VERTEX_POINT ( 'NONE', #26967 ) ;
#96313=LINE ( 'NONE', #115907, #96919 ) ;
#96542=AXIS2_PLACEMENT_3D ( 'NONE', #201944, #204487, #122407 ) ;
#96615=VECTOR ( 'NONE', #53494, 1000.000000000000227 ) ;
#96680=ORIENTED_EDGE ( 'NONE', *, *, #151024, .F. ) ;
#96919=VECTOR ( 'NONE', #101415, 1000.000000000000227 ) ;
#97070=EDGE_CURVE ( 'NONE', #155655, #182610, #204218, .T. ) ;
#97280=EDGE_CURVE ( 'NONE', #117708, #235384, #104650, .T. ) ;
#97309=CARTESIAN_POINT ( 'NONE',  ( 14.87567385445976598, 12.45583213463953420, -213.8748143118951646 ) ) ;
#97589=FACE_OUTER_BOUND ( 'NONE', #170004, .T. ) ;
#97698=DIRECTION ( 'NONE',  ( -0.000000000000000000, 0.2128009952263603677, -0.9770955615653313941 ) ) ;
#97772=CARTESIAN_POINT ( 'NONE',  ( 13.43663047529819821, 13.14811317477304442, -216.9788617421937147 ) ) ;
#97826=ORIENTED_EDGE ( 'NONE', *, *, #98055, .F. ) ;
#97902=CARTESIAN_POINT ( 'NONE',  ( -16.87683809663752399, 13.94542889413352604, -218.6696862871272060 ) ) ;
#97935=CARTESIAN_POINT ( 'NONE',  ( -16.93906926870270624, 12.45421141385810770, -211.1353277132250241 ) ) ;
#98055=EDGE_CURVE ( 'NONE', #171657, #234584, #79858, .T. ) ;
#98221=VECTOR ( 'NONE', #198657, 1000.000000000000227 ) ;
#98240=EDGE_CURVE ( 'NONE', #190315, #200838, #154844, .T. ) ;
#98245=CARTESIAN_POINT ( 'NONE',  ( -16.78805706634180694, 14.15604990364249716, -219.2497315528685249 ) ) ;
#98285=AXIS2_PLACEMENT_3D ( 'NONE', #94716, #171728, #152163 ) ;
#98345=ORIENTED_EDGE ( 'NONE', *, *, #135217, .F. ) ;
#98604=CARTESIAN_POINT ( 'NONE',  ( 17.23472005113827876, 14.76331920405063869, -220.3480848590899654 ) ) ;
#98652=EDGE_LOOP ( 'NONE', ( #196988, #181725, #43649, #1650 ) ) ;
#98873=CARTESIAN_POINT ( 'NONE',  ( -16.79270642812254977, 12.41271867757595260, -211.2545014300695243 ) ) ;
#99037=ORIENTED_EDGE ( 'NONE', *, *, #93165, .T. ) ;
#99074=EDGE_CURVE ( 'NONE', #34114, #91388, #158359, .T. ) ;
#99227=CARTESIAN_POINT ( 'NONE',  ( -16.94309007106719633, 12.44588479347206622, -211.1907070338996277 ) ) ;
#99258=DIRECTION ( 'NONE',  ( 0.000000000000000000, -0.9770955615653551529, -0.2128009952262517601 ) ) ;
#99427=DIRECTION ( 'NONE',  ( -0.000000000000000000, 0.2128009952263603677, -0.9770955615653313941 ) ) ;
#99497=ORIENTED_EDGE ( 'NONE', *, *, #64115, .T. ) ;
#100015=CARTESIAN_POINT ( 'NONE',  ( -20.65000000000000568, 9.775875410973588586, -211.8174516384118817 ) ) ;
#100086=CARTESIAN_POINT ( 'NONE',  ( -16.92989507731676824, 14.10952512909879530, -219.0278967931764385 ) ) ;
#100105=CARTESIAN_POINT ( 'NONE',  ( -14.00000000000000178, 13.18880795147152440, -215.2702608532411830 ) ) ;
#100219=CARTESIAN_POINT ( 'NONE',  ( 18.54999999999999716, 11.24151875332162831, -211.4982501455723138 ) ) ;
#100231=ORIENTED_EDGE ( 'NONE', *, *, #184433, .F. ) ;
#100302=VECTOR ( 'NONE', #139060, 1000.000000000000000 ) ;
#100419=CARTESIAN_POINT ( 'NONE',  ( -16.87331047859649757, 14.15900158805613884, -219.2550725561364118 ) ) ;
#100475=CARTESIAN_POINT ( 'NONE',  ( -16.84793658983437581, 14.14120149177083263, -219.1733417585090820 ) ) ;
#100496=VERTEX_POINT ( 'NONE', #37833 ) ;
#100524=EDGE_CURVE ( 'NONE', #94156, #233837, #56056, .T. ) ;
#100527=LINE ( 'NONE', #203524, #182107 ) ;
#100554=ADVANCED_FACE ( 'NONE', ( #121234 ), #24688, .F. ) ;
#100760=CARTESIAN_POINT ( 'NONE',  ( -16.94445028196807002, 14.20918193489391790, -219.2878138714100373 ) ) ;
#100840=LINE ( 'NONE', #240408, #21558 ) ;
#101096=FACE_OUTER_BOUND ( 'NONE', #122091, .T. ) ;
#101415=DIRECTION ( 'NONE',  ( -0.000000000000000000, 0.2128009952263603677, -0.9770955615653313941 ) ) ;
#101437=CARTESIAN_POINT ( 'NONE',  ( -16.77977881697927032, 12.41313456322023967, -211.2547300165144009 ) ) ;
#101449=EDGE_LOOP ( 'NONE', ( #190549, #2857, #187749, #68480 ) ) ;
#101454=CARTESIAN_POINT ( 'NONE',  ( -17.04761207306817994, 12.48873323627475074, -211.2266201293557231 ) ) ;
#101456=VERTEX_POINT ( 'NONE', #9291 ) ;
#101614=DIRECTION ( 'NONE',  ( 1.000000000000000000, 0.000000000000000000, 0.000000000000000000 ) ) ;
#101660=VERTEX_POINT ( 'NONE', #20877 ) ;
#101704=ORIENTED_EDGE ( 'NONE', *, *, #205105, .T. ) ;
#101728=CARTESIAN_POINT ( 'NONE',  ( -16.77683809663752257, 26.68086916408615750, -212.3318337774905160 ) ) ;
#101757=LINE ( 'NONE', #237456, #240836 ) ;
#102031=AXIS2_PLACEMENT_3D ( 'NONE', #237956, #59283, #16373 ) ;
#102066=CARTESIAN_POINT ( 'NONE',  ( -16.90987985657661952, 14.17073459112586598, -219.2722564374412286 ) ) ;
#102274=ORIENTED_EDGE ( 'NONE', *, *, #151024, .T. ) ;
#102397=CARTESIAN_POINT ( 'NONE',  ( -16.90202395485622944, 14.18586230441212770, -219.3034790129322289 ) ) ;
#102418=DIRECTION ( 'NONE',  ( 1.186688945009010077E-16, -0.9770955615653316162, -0.2128009952263604232 ) ) ;
#102436=ORIENTED_EDGE ( 'NONE', *, *, #60324, .T. ) ;
#102545=CIRCLE ( 'NONE', #135712, 0.1000000000000032530 ) ;
#102690=CARTESIAN_POINT ( 'NONE',  ( 20.99999999999999645, 12.21861431488691707, -211.2854491503459826 ) ) ;
#102898=CARTESIAN_POINT ( 'NONE',  ( -16.87683809663752399, 26.68086916408615750, -212.3318337774905160 ) ) ;
#103058=CARTESIAN_POINT ( 'NONE',  ( -16.86578989773640913, 14.21741489235582634, -219.3597035475708594 ) ) ;
#103318=EDGE_CURVE ( 'NONE', #180552, #103723, #43929, .T. ) ;
#103352=VERTEX_POINT ( 'NONE', #204330 ) ;
#103572=VERTEX_POINT ( 'NONE', #154674 ) ;
#103723=VERTEX_POINT ( 'NONE', #64525 ) ;
#103930=ORIENTED_EDGE ( 'NONE', *, *, #100524, .F. ) ;
#103945=ORIENTED_EDGE ( 'NONE', *, *, #233745, .T. ) ;
#104007=ORIENTED_EDGE ( 'NONE', *, *, #43207, .T. ) ;
#104028=ORIENTED_EDGE ( 'NONE', *, *, #59514, .T. ) ;
#104186=CARTESIAN_POINT ( 'NONE',  ( -17.11825945287481332, 14.13772148853350252, -219.1573629999798811 ) ) ;
#104204=DIRECTION ( 'NONE',  ( 0.000000000000000000, -0.9770955615653315052, -0.2128009952263603954 ) ) ;
#104329=VERTEX_POINT ( 'NONE', #56845 ) ;
#104576=CARTESIAN_POINT ( 'NONE',  ( -16.85718274719434007, 12.42113698003434585, -211.1526569265139699 ) ) ;
#104637=EDGE_CURVE ( 'NONE', #82079, #113827, #256009, .T. ) ;
#104650=LINE ( 'NONE', #202507, #63403 ) ;
#104656=EDGE_LOOP ( 'NONE', ( #86529, #133210, #56232, #122905, #27937 ) ) ;
#105174=CARTESIAN_POINT ( 'NONE',  ( -16.89268316805465986, 14.16190809729244648, -219.2603268738197073 ) ) ;
#105183=DIRECTION ( 'NONE',  ( -1.000000000000000000, 1.614276770400120371E-15, 3.515722686956159758E-16 ) ) ;
#105466=CARTESIAN_POINT ( 'NONE',  ( -12.33960340485503515, 12.83090422469975778, -215.9260128953783067 ) ) ;
#105482=AXIS2_PLACEMENT_3D ( 'NONE', #39836, #119354, #61946 ) ;
#105744=EDGE_LOOP ( 'NONE', ( #100231, #221744, #186559, #109842 ) ) ;
#105863=CARTESIAN_POINT ( 'NONE',  ( -16.92778301347309622, 12.44710274780528181, -211.1553281274974552 ) ) ;
#105956=B_SPLINE_CURVE_WITH_KNOTS ( 'NONE', 3,
 ( #123942, #62680, #26125, #223012, #166944, #202183, #65229, #144752, #103058, #225568 ),
 .UNSPECIFIED., .F., .F.,
 ( 4, 3, 3, 4 ),
 ( 7.632826238685023174E-06, 4.756916949876414344E-05, 9.484459048151255107E-05, 0.0001435500935099816788 ),
 .UNSPECIFIED. ) ;
#106152=LINE ( 'NONE', #162313, #201776 ) ;
#106301=CIRCLE ( 'NONE', #139625, 1.500000000000001332 ) ;
#106547=CARTESIAN_POINT ( 'NONE',  ( -18.34374000495059676, 16.37079970714665933, -222.2530670965321349 ) ) ;
#106549=CARTESIAN_POINT ( 'NONE',  ( -16.83199318825828783, 14.11404101182791493, -219.1395801100928793 ) ) ;
#106564=VERTEX_POINT ( 'NONE', #205785 ) ;
#106575=CARTESIAN_POINT ( 'NONE',  ( 20.73486653747088937, 12.00939135261245028, -219.7232347456343859 ) ) ;
#106593=ORIENTED_EDGE ( 'NONE', *, *, #143802, .F. ) ;
#106600=CARTESIAN_POINT ( 'NONE',  ( -16.80438519320023616, 12.41397469025448785, -211.2436573308034440 ) ) ;
#106613=CARTESIAN_POINT ( 'NONE',  ( -16.88328101497759448, 14.15959734275620541, -219.2561499714656748 ) ) ;
#106694=PLANE ( 'NONE',  #162984 ) ;
#106713=VECTOR ( 'NONE', #37304, 1000.000000000000227 ) ;
#106758=CARTESIAN_POINT ( 'NONE',  ( -17.01473183483381035, 14.13772148853350252, -219.1573629999798811 ) ) ;
#107005=VECTOR ( 'NONE', #109285, 1000.000000000000227 ) ;
#107200=ORIENTED_EDGE ( 'NONE', *, *, #223928, .T. ) ;
#107272=CARTESIAN_POINT ( 'NONE',  ( -17.11825945287482753, 12.51174298335651791, -211.2216088517780577 ) ) ;
#107315=CARTESIAN_POINT ( 'NONE',  ( -18.40000000000000213, 13.88102806299823833, -210.8210490262177359 ) ) ;
#107555=EDGE_LOOP ( 'NONE', ( #88543, #189702, #121458 ) ) ;
#107850=FILL_AREA_STYLE_COLOUR ( '', #220047 ) ;
#107875=DIRECTION ( 'NONE',  ( -1.073024830501117725E-15, -0.2128009952263604232, 0.9770955615653316162 ) ) ;
#107997=ADVANCED_FACE ( 'NONE', ( #124649 ), #140013, .T. ) ;
#108053=ORIENTED_EDGE ( 'NONE', *, *, #48345, .T. ) ;
#108083=CARTESIAN_POINT ( 'NONE',  ( -12.24999999999999822, 12.72489043187539970, -215.4897534858791914 ) ) ;
#108214=AXIS2_PLACEMENT_3D ( 'NONE', #256045, #94455, #119170 ) ;
#108863=EDGE_CURVE ( 'NONE', #210898, #203112, #133970, .T. ) ;
#108903=CARTESIAN_POINT ( 'NONE',  ( -16.92989143108097494, 12.46350622712228429, -211.4700479134609736 ) ) ;
#108962=VECTOR ( 'NONE', #146824, 1000.000000000000000 ) ;
#109189=CARTESIAN_POINT ( 'NONE',  ( -16.87331047859649757, 14.15900158805613884, -219.2550725561364118 ) ) ;
#109285=DIRECTION ( 'NONE',  ( 0.000000000000000000, 0.9770955615653313941, 0.2128009952263603677 ) ) ;
#109325=FACE_OUTER_BOUND ( 'NONE', #86007, .T. ) ;
#109335=FACE_OUTER_BOUND ( 'NONE', #91936, .T. ) ;
#109371=DIRECTION ( 'NONE',  ( -1.000000000000000000, 0.000000000000000000, 0.000000000000000000 ) ) ;
#109644=CARTESIAN_POINT ( 'NONE',  ( -16.87851181299898684, 12.41404482784453656, -211.2427395888011006 ) ) ;
#109830=VERTEX_POINT ( 'NONE', #121534 ) ;
#109842=ORIENTED_EDGE ( 'NONE', *, *, #236076, .F. ) ;
#110025=EDGE_CURVE ( 'NONE', #205524, #231927, #130479, .T. ) ;
#110366=CARTESIAN_POINT ( 'NONE',  ( 18.54999999999999716, 12.98648691417778167, -219.5104337504080263 ) ) ;
#110610=DIRECTION ( 'NONE',  ( -1.000000000000000000, 0.000000000000000000, 0.000000000000000000 ) ) ;
#110937=CARTESIAN_POINT ( 'NONE',  ( -18.34374000495060386, 13.17878477875124688, -207.5966336730521391 ) ) ;
#111410=FACE_OUTER_BOUND ( 'NONE', #10814, .T. ) ;
#112090=CIRCLE ( 'NONE', #241273, 0.09999999999999810429 ) ;
#112597=EDGE_CURVE ( 'NONE', #196416, #183798, #183351, .T. ) ;
#112667=VECTOR ( 'NONE', #242619, 1000.000000000000114 ) ;
#112695=CARTESIAN_POINT ( 'NONE',  ( -16.95709691156223542, 14.15686132874403214, -219.2452453564496295 ) ) ;
#112753=ORIENTED_EDGE ( 'NONE', *, *, #229731, .F. ) ;
#112777=ORIENTED_EDGE ( 'NONE', *, *, #110025, .F. ) ;
#112987=VERTEX_POINT ( 'NONE', #24326 ) ;
#113150=CARTESIAN_POINT ( 'NONE',  ( -16.93262454970419384, 14.22623245403305070, -219.3193133873473641 ) ) ;
#113720=DIRECTION ( 'NONE',  ( -1.000000000000000000, -0.000000000000000000, -0.000000000000000000 ) ) ;
#113813=DIRECTION ( 'NONE',  ( 0.000000000000000000, 0.9770955615653313941, 0.2128009952263603677 ) ) ;
#113827=VERTEX_POINT ( 'NONE', #147162 ) ;
#113949=DIRECTION ( 'NONE',  ( 0.000000000000000000, -0.9770955615653315052, -0.2128009952263603954 ) ) ;
#114009=EDGE_LOOP ( 'NONE', ( #247412, #216669, #215302, #79536 ) ) ;
#114251=CARTESIAN_POINT ( 'NONE',  ( -18.40000000000000213, 13.90230816252087642, -210.9187585823742666 ) ) ;
#114298=DIRECTION ( 'NONE',  ( -1.020425574104003999E-15, -0.2128009952263603677, 0.9770955615653313941 ) ) ;
#114620=CARTESIAN_POINT ( 'NONE',  ( -16.88705144915432754, 12.47382595179198184, -211.5174318890890390 ) ) ;
#114733=LINE ( 'NONE', #135559, #4263 ) ;
#114756=DIRECTION ( 'NONE',  ( 0.000000000000000000, -0.2128009952263603677, 0.9770955615653313941 ) ) ;
#114807=CARTESIAN_POINT ( 'NONE',  ( 13.77030915526558275, 13.17382239637293040, -217.0529139566851597 ) ) ;
#115007=EDGE_LOOP ( 'NONE', ( #176092, #178351, #84099, #162019 ) ) ;
#115102=CARTESIAN_POINT ( 'NONE',  ( 23.24999999999999645, 9.957490673325210651, -220.1701168356097469 ) ) ;
#115251=CARTESIAN_POINT ( 'NONE',  ( -17.01825945287481545, 14.13772148853350252, -219.1573629999798811 ) ) ;
#115609=CARTESIAN_POINT ( 'NONE',  ( 18.39999999999998082, 13.17878477875124865, -207.5966336730521391 ) ) ;
#115881=ORIENTED_EDGE ( 'NONE', *, *, #58971, .T. ) ;
#115901=B_SPLINE_CURVE_WITH_KNOTS ( 'NONE', 3,
 ( #234751, #195650, #174830, #56085, #13149, #15736, #92668, #253023, #95238, #134346, #36590, #251748, #256822, #172261, #114807, #93952, #97772, #18272, #177381, #73147, #193073, #151387, #37859, #152683, #74435, #135638, #215188, #153984, #233491, #116100 ),
 .UNSPECIFIED., .F., .F.,
 ( 4, 2, 2, 2, 2, 2, 2, 2, 2, 2, 2, 2, 2, 2, 4 ),
 ( 0.000000000000000000, 0.0003422764154113345906, 0.0006845528308226691812, 0.001026829246234003826, 0.001369105661645338362, 0.002053658492468006351, 0.002738211323290674556, 0.003080487738702008659, 0.003422764154113342328, 0.003765040569524676431, 0.004107316984936010100, 0.004449593400347344636, 0.004791869815758678305, 0.005134146231170011974, 0.005476422646581346511 ),
 .UNSPECIFIED. ) ;
#115907=CARTESIAN_POINT ( 'NONE',  ( 23.24999999999999645, 13.44928205424795564, -207.5377222505711075 ) ) ;
#115915=CARTESIAN_POINT ( 'NONE',  ( -16.89935556175678855, 12.51823704456101005, -211.7213495520792037 ) ) ;
#115999=CARTESIAN_POINT ( 'NONE',  ( -17.11825945287482753, 12.43531352672262003, -211.3405985074572300 ) ) ;
#116067=SHAPE_DEFINITION_REPRESENTATION ( #207591, #233377 ) ;
#116100=CARTESIAN_POINT ( 'NONE',  ( 12.25000000000000000, 12.70026017068886937, -215.3766613508543628 ) ) ;
#116238=CIRCLE ( 'NONE', #74758, 14.30833333333333890 ) ;
#116408=PLANE ( 'NONE',  #182601 ) ;
#116489=ADVANCED_FACE ( 'NONE', ( #73927 ), #54312, .F. ) ;
#116538=DIRECTION ( 'NONE',  ( -1.000000000000000000, 0.000000000000000000, 0.000000000000000000 ) ) ;
#116708=VECTOR ( 'NONE', #97698, 1000.000000000000227 ) ;
#117056=PLANE ( 'NONE',  #57257 ) ;
#117193=CARTESIAN_POINT ( 'NONE',  ( -16.83233564386407366, 12.42141036011986621, -211.3697030754569255 ) ) ;
#117708=VERTEX_POINT ( 'NONE', #72678 ) ;
#117805=FACE_OUTER_BOUND ( 'NONE', #13040, .T. ) ;
#117820=DIRECTION ( 'NONE',  ( 1.073024830501117725E-15, 0.2128009952263604232, -0.9770955615653316162 ) ) ;
#117849=CYLINDRICAL_SURFACE ( 'NONE', #248942, 0.1000000000000054040 ) ;
#117947=EDGE_CURVE ( 'NONE', #58136, #55301, #116238, .T. ) ;
#118197=CARTESIAN_POINT ( 'NONE',  ( 15.74999999999999645, 12.70026017068886226, -215.3766613508543628 ) ) ;
#118568=ADVANCED_FACE ( 'NONE', ( #74931 ), #35796, .F. ) ;
#118689=ORIENTED_EDGE ( 'NONE', *, *, #255720, .T. ) ;
#118834=CARTESIAN_POINT ( 'NONE',  ( -16.94062896051973865, 12.44566954809400627, -211.1874024072765792 ) ) ;
#118885=CARTESIAN_POINT ( 'NONE',  ( 20.09999999999999787, 12.21861431488691530, -211.2854491503459826 ) ) ;
#119101=EDGE_LOOP ( 'NONE', ( #150863, #234173, #57572, #211185, #40855, #199248, #4710, #129658, #245140 ) ) ;
#119125=VERTEX_POINT ( 'NONE', #64027 ) ;
#119170=DIRECTION ( 'NONE',  ( 0.5932847527679309119, -0.7865547670005532677, -0.1713032417725953160 ) ) ;
#119354=DIRECTION ( 'NONE',  ( 1.186688945009010077E-16, -0.9770955615653316162, -0.2128009952263604232 ) ) ;
#119691=VECTOR ( 'NONE', #32148, 1000.000000000000227 ) ;
#119831=CARTESIAN_POINT ( 'NONE',  ( -15.70407651835961360, 12.60827992760467531, -214.9270390227368352 ) ) ;
#120011=ORIENTED_EDGE ( 'NONE', *, *, #86774, .F. ) ;
#120091=ORIENTED_EDGE ( 'NONE', *, *, #202271, .F. ) ;
#120108=CARTESIAN_POINT ( 'NONE',  ( -16.84981964351492323, 14.08033693763356986, -219.0474555060754085 ) ) ;
#120256=B_SPLINE_CURVE_WITH_KNOTS ( 'NONE', 3,
 ( #28593, #108083, #7704, #165494, #105466, #127644, #45533, #125083, #66383, #5085, #248875, #70264, #123792, #168095, #225430, #207189, #187629, #88481, #8972, #228024, #205882, #203327, #186338, #204594, #166799, #148493, #208481, #183763, #67660, #224157 ),
 .UNSPECIFIED., .F., .F.,
 ( 4, 2, 2, 2, 2, 2, 2, 2, 2, 2, 2, 2, 2, 2, 4 ),
 ( 0.000000000000000000, 0.0003422764154113365422, 0.0006845528308226730843, 0.001026829246234009464, 0.001369105661645346169, 0.002053658492468014591, 0.002738211323290683230, 0.003080487738702017333, 0.003422764154113351436, 0.003765040569524685538, 0.004107316984936019641, 0.004449593400347353310, 0.004791869815758687846, 0.005134146231170021515, 0.005476422646581355184 ),
 .UNSPECIFIED. ) ;
#120296=ADVANCED_FACE ( 'NONE', ( #69226 ), #210008, .F. ) ;
#120426=EDGE_CURVE ( 'NONE', #183798, #202859, #216409, .T. ) ;
#120870=VECTOR ( 'NONE', #22543, 1000.000000000000000 ) ;
#120901=LINE ( 'NONE', #82986, #279 ) ;
#120907=EDGE_CURVE ( 'NONE', #104329, #205524, #239529, .T. ) ;
#120959=CARTESIAN_POINT ( 'NONE',  ( -21.65000000000000213, 11.52084357182974195, -219.8296352432475942 ) ) ;
#120976=CARTESIAN_POINT ( 'NONE',  ( -21.64999999999999858, 14.23543104469003673, -219.1360829004572395 ) ) ;
#121014=EDGE_LOOP ( 'NONE', ( #21414, #138794, #104028, #29324 ) ) ;
#121051=AXIS2_PLACEMENT_3D ( 'NONE', #106575, #107875, #226517 ) ;
#121053=EDGE_CURVE ( 'NONE', #21362, #55330, #165122, .T. ) ;
#121076=DIRECTION ( 'NONE',  ( -1.000000000000000000, -0.000000000000000000, -0.000000000000000000 ) ) ;
#121102=DIRECTION ( 'NONE',  ( 1.000000000000000000, 0.000000000000000000, 0.000000000000000000 ) ) ;
#121107=ORIENTED_EDGE ( 'NONE', *, *, #213571, .F. ) ;
#121140=DIRECTION ( 'NONE',  ( 1.000000000000000000, 0.000000000000000000, 0.000000000000000000 ) ) ;
#121234=FACE_OUTER_BOUND ( 'NONE', #80705, .T. ) ;
#121398=CARTESIAN_POINT ( 'NONE',  ( -16.85697194749124250, 14.05784564333523079, -218.9854180901164113 ) ) ;
#121458=ORIENTED_EDGE ( 'NONE', *, *, #16144, .T. ) ;
#121534=CARTESIAN_POINT ( 'NONE',  ( -18.40000000000000213, 16.38400329561159907, -222.2501914957450424 ) ) ;
#121972=DIRECTION ( 'NONE',  ( -1.073024830501117725E-15, -0.2128009952263604232, 0.9770955615653316162 ) ) ;
#122003=CARTESIAN_POINT ( 'NONE',  ( -16.86445178670650691, 14.17961099607968833, -219.2923173631047860 ) ) ;
#122031=CIRCLE ( 'NONE', #246924, 1.749999999999998002 ) ;
#122091=EDGE_LOOP ( 'NONE', ( #256973, #180174, #144106, #128063 ) ) ;
#122230=ORIENTED_EDGE ( 'NONE', *, *, #143842, .F. ) ;
#122277=ORIENTED_EDGE ( 'NONE', *, *, #147720, .F. ) ;
#122407=DIRECTION ( 'NONE',  ( 0.000000000000000000, -0.2128009952263603677, 0.9770955615653313941 ) ) ;
#122499=CARTESIAN_POINT ( 'NONE',  ( -16.92507428761700794, 14.14551054555384901, -219.1931271797256784 ) ) ;
#122519=CYLINDRICAL_SURFACE ( 'NONE', #122731, 14.30833333333333535 ) ;
#122659=CARTESIAN_POINT ( 'NONE',  ( -16.77180007708460252, 14.16206291785975857, -219.2691289366548517 ) ) ;
#122731=AXIS2_PLACEMENT_3D ( 'NONE', #82058, #101614, #140785 ) ;
#122905=ORIENTED_EDGE ( 'NONE', *, *, #246825, .F. ) ;
#122936=ORIENTED_EDGE ( 'NONE', *, *, #12892, .F. ) ;
#122951=CARTESIAN_POINT ( 'NONE',  ( -16.94275863006528482, 14.20646624631278065, -219.2874100846283625 ) ) ;
#123031=DIRECTION ( 'NONE',  ( -1.000000000000000000, 0.000000000000000000, -0.000000000000000000 ) ) ;
#123610=ADVANCED_FACE ( 'NONE', ( #224266 ), #209997, .T. ) ;
#123614=LINE ( 'NONE', #181031, #36786 ) ;
#123792=CARTESIAN_POINT ( 'NONE',  ( -13.77083647240106323, 13.17759476088265203, -217.0636392655389102 ) ) ;
#123942=CARTESIAN_POINT ( 'NONE',  ( -16.89268316805465986, 14.16190809729244648, -219.2603268738197073 ) ) ;
#124240=CARTESIAN_POINT ( 'NONE',  ( -16.91776028072577631, 14.17742018842817942, -219.2766717927335378 ) ) ;
#124375=DIRECTION ( 'NONE',  ( -0.000000000000000000, 0.2128009952263603677, -0.9770955615653313941 ) ) ;
#124453=PLANE ( 'NONE',  #82328 ) ;
#124456=ORIENTED_EDGE ( 'NONE', *, *, #213571, .T. ) ;
#124628=CARTESIAN_POINT ( 'NONE',  ( -16.97048326478264002, 12.51854146005355872, -211.7227473041271253 ) ) ;
#124649=FACE_OUTER_BOUND ( 'NONE', #139062, .T. ) ;
#124719=LINE ( 'NONE', #84241, #108962 ) ;
#124881=EDGE_LOOP ( 'NONE', ( #223815, #213155, #64269, #253846 ) ) ;
#125008=FACE_OUTER_BOUND ( 'NONE', #257275, .T. ) ;
#125083=CARTESIAN_POINT ( 'NONE',  ( -12.60829076262180948, 12.96596579538268834, -216.4109158611324233 ) ) ;
#125288=ORIENTED_EDGE ( 'NONE', *, *, #110025, .T. ) ;
#125384=FACE_OUTER_BOUND ( 'NONE', #124881, .T. ) ;
#125427=CARTESIAN_POINT ( 'NONE',  ( -16.27683809663750480, 11.10425270649115603, -208.0484446391143649 ) ) ;
#125757=LINE ( 'NONE', #61949, #140257 ) ;
#125821=ORIENTED_EDGE ( 'NONE', *, *, #77794, .F. ) ;
#125845=EDGE_LOOP ( 'NONE', ( #146695, #141353, #175545, #140837, #189577 ) ) ;
#125974=VERTEX_POINT ( 'NONE', #16359 ) ;
#125982=DIRECTION ( 'NONE',  ( -1.000000000000000000, 0.000000000000000000, 0.000000000000000000 ) ) ;
#126063=LINE ( 'NONE', #141782, #142350 ) ;
#126172=CARTESIAN_POINT ( 'NONE',  ( -16.81744102076749314, 12.41403342719998726, -211.2428889513006993 ) ) ;
#126214=CARTESIAN_POINT ( 'NONE',  ( -12.84409460144754433, 12.47889858296947807, -214.0750992090278260 ) ) ;
#126231=VECTOR ( 'NONE', #39845, 1000.000000000000227 ) ;
#126395=CARTESIAN_POINT ( 'NONE',  ( -17.22767730083581839, 12.52910306356951686, -209.8951030483589193 ) ) ;
#126455=DIRECTION ( 'NONE',  ( 1.000000000000000000, 1.159508501126949537E-16, 2.525285885220370376E-17 ) ) ;
#126459=VECTOR ( 'NONE', #127942, 1000.000000000000000 ) ;
#126548=DIRECTION ( 'NONE',  ( 1.000000000000000000, 0.000000000000000000, 0.000000000000000000 ) ) ;
#126843=CARTESIAN_POINT ( 'NONE',  ( -16.97092634996727867, 12.45953117125834453, -211.2126573136994523 ) ) ;
#126918=VECTOR ( 'NONE', #49573, 1000.000000000000341 ) ;
#127340=VECTOR ( 'NONE', #216203, 1000.000000000000227 ) ;
#127473=CARTESIAN_POINT ( 'NONE',  ( -16.77779411503079388, 12.41300279975761889, -211.2564769120770336 ) ) ;
#127513=CARTESIAN_POINT ( 'NONE',  ( -12.47155713865591586, 12.53760658702567810, -214.5091953838863503 ) ) ;
#127536=FACE_OUTER_BOUND ( 'NONE', #18968, .T. ) ;
#127610=PLANE ( 'NONE',  #243013 ) ;
#127612=AXIS2_PLACEMENT_3D ( 'NONE', #235341, #56680, #136222 ) ;
#127644=CARTESIAN_POINT ( 'NONE',  ( -12.42749937872395627, 12.88570875296796459, -216.1309391439169758 ) ) ;
#127764=EDGE_CURVE ( 'NONE', #209959, #210119, #237389, .T. ) ;
#127791=CARTESIAN_POINT ( 'NONE',  ( -12.25000000000000178, 13.18880795147152440, -215.2702608532411830 ) ) ;
#127942=DIRECTION ( 'NONE',  ( -1.000000000000000000, 0.000000000000000000, -0.000000000000000000 ) ) ;
#127951=ORIENTED_EDGE ( 'NONE', *, *, #167239, .F. ) ;
#128063=ORIENTED_EDGE ( 'NONE', *, *, #233745, .F. ) ;
#128357=FACE_OUTER_BOUND ( 'NONE', #241769, .T. ) ;
#128478=CARTESIAN_POINT ( 'NONE',  ( -16.84421487269769102, 12.41818349826529477, -211.2619443885827764 ) ) ;
#128712=CARTESIAN_POINT ( 'NONE',  ( -16.80469485234340610, 14.14281391749209860, -219.2176264709205498 ) ) ;
#128781=CARTESIAN_POINT ( 'NONE',  ( -16.89146115310546392, 14.16143799253418400, -219.2594773961805288 ) ) ;
#128857=EDGE_LOOP ( 'NONE', ( #33752, #185803 ) ) ;
#129003=CARTESIAN_POINT ( 'NONE',  ( 13.99999999999999822, 13.18880795147152618, -215.2702608532411830 ) ) ;
#129126=B_SPLINE_CURVE_WITH_KNOTS ( 'NONE', 3,
 ( #208635, #189056, #10426, #89938, #70429, #149948, #44420 ),
 .UNSPECIFIED., .F., .F.,
 ( 4, 3, 4 ),
 ( 0.000000000000000000, 4.520325912680733322E-05, 5.794988040901469109E-05 ),
 .UNSPECIFIED. ) ;
#129139=EDGE_LOOP ( 'NONE', ( #104007, #97826, #15935, #77952, #153620 ) ) ;
#129195=CARTESIAN_POINT ( 'NONE',  ( -16.86422026484316916, 12.41958735970269956, -211.1723035762320535 ) ) ;
#129273=DIRECTION ( 'NONE',  ( 0.000000000000000000, 0.2128009952263603677, -0.9770955615653313941 ) ) ;
#129410=CARTESIAN_POINT ( 'NONE',  ( -17.11825945287482753, 12.43531352672261825, -211.3405985074572300 ) ) ;
#129658=ORIENTED_EDGE ( 'NONE', *, *, #60324, .F. ) ;
#129719=DIRECTION ( 'NONE',  ( -0.000000000000000000, 0.2128009952263603677, -0.9770955615653313941 ) ) ;
#129756=CARTESIAN_POINT ( 'NONE',  ( -16.97683809663752186, 12.57413723904469904, -211.9780204941619104 ) ) ;
#129926=ORIENTED_EDGE ( 'NONE', *, *, #73307, .F. ) ;
#130131=AXIS2_PLACEMENT_3D ( 'NONE', #160350, #178630, #222847 ) ;
#130134=ADVANCED_FACE ( 'NONE', ( #229791 ), #46327, .T. ) ;
#130228=VECTOR ( 'NONE', #196546, 1000.000000000000000 ) ;
#130260=LINE ( 'NONE', #88557, #67165 ) ;
#130430=DIRECTION ( 'NONE',  ( -0.000000000000000000, 0.2128009952263604232, -0.9770955615653316162 ) ) ;
#130461=CARTESIAN_POINT ( 'NONE',  ( 12.25000000000000000, 13.18880795147152618, -215.2702608532411830 ) ) ;
#130464=CARTESIAN_POINT ( 'NONE',  ( -16.89268316805466341, 12.41449167011727361, -211.2369018264743090 ) ) ;
#130479=LINE ( 'NONE', #172232, #145201 ) ;
#130688=CARTESIAN_POINT ( 'NONE',  ( -17.01764560440165397, 12.43531352655448430, -211.3405985066852395 ) ) ;
#131015=( NAMED_UNIT ( * ) SI_UNIT ( $, .STERADIAN. ) SOLID_ANGLE_UNIT ( ) );
#131613=DIRECTION ( 'NONE',  ( 0.000000000000000000, 0.9770955615653313941, 0.2128009952263603677 ) ) ;
#131662=ADVANCED_FACE ( 'NONE', ( #242669 ), #41934, .F. ) ;
#131786=CARTESIAN_POINT ( 'NONE',  ( -16.89268316805466341, 12.41449167011727361, -211.2369018264743090 ) ) ;
#132113=ADVANCED_FACE ( 'NONE', ( #125008 ), #106694, .F. ) ;
#132618=VECTOR ( 'NONE', #55783, 1000.000000000000227 ) ;
#132638=ORIENTED_EDGE ( 'NONE', *, *, #251024, .F. ) ;
#132659=DIRECTION ( 'NONE',  ( 0.000000000000000000, 0.9770955615653313941, 0.2128009952263603677 ) ) ;
#132730=CARTESIAN_POINT ( 'NONE',  ( -16.94107738177414291, 14.24304960796391306, -219.3391119284832484 ) ) ;
#132761=CARTESIAN_POINT ( 'NONE',  ( -15.75000000000000355, 13.18880795147152440, -215.2702608532411830 ) ) ;
#133210=ORIENTED_EDGE ( 'NONE', *, *, #150062, .T. ) ;
#133303=DIRECTION ( 'NONE',  ( -1.000000000000000000, -0.000000000000000000, -0.000000000000000000 ) ) ;
#133536=CARTESIAN_POINT ( 'NONE',  ( -16.97092634996651839, 14.21295061030198781, -219.2636457483668835 ) ) ;
#133717=DIRECTION ( 'NONE',  ( 0.000000000000000000, 0.9963347912923393723, -0.08553936906741056723 ) ) ;
#133805=LINE ( 'NONE', #114251, #106713 ) ;
#133861=DIRECTION ( 'NONE',  ( -1.000000000000000000, 2.171475777237622503E-16, -9.970532993647777410E-16 ) ) ;
#133970=LINE ( 'NONE', #11482, #61287 ) ;
#133984=( BOUNDED_SURFACE ( )  B_SPLINE_SURFACE ( 3, 2, ( 
 ( #56470, #19952, #4209 ),
 ( #105863, #45916, #104576 ),
 ( #40814, #242826, #245415 ),
 ( #181596, #85012, #142444 ) ),
 .UNSPECIFIED., .F., .F., .T. ) 
 B_SPLINE_SURFACE_WITH_KNOTS ( ( 4, 4 ),
 ( 3, 3 ),
 ( 0.0008258556059633580639, 0.0009616864997632887033 ),
 ( 0.000000000000000000, 1.000000000000000000 ),
 .UNSPECIFIED. ) 
 GEOMETRIC_REPRESENTATION_ITEM ( )  RATIONAL_B_SPLINE_SURFACE ( (
 ( 1.000000000000000000, 0.9152888060719308605, 1.000000000000000000),
 ( 1.000000000000000000, 0.9327727094137928665, 1.000000000000000000),
 ( 1.000000000000000000, 0.9369023509258854743, 1.000000000000000000),
 ( 1.000000000000000000, 0.9246339933864360372, 1.000000000000000000) ) ) 
 REPRESENTATION_ITEM ( '' )  SURFACE ( )  );
#133990=CARTESIAN_POINT ( 'NONE',  ( -16.93589915522259304, 14.23555534794845023, -219.3310829164208542 ) ) ;
#134173=CARTESIAN_POINT ( 'NONE',  ( -16.87333278164151196, 12.45100533682980348, -211.7293307750952920 ) ) ;
#134234=CARTESIAN_POINT ( 'NONE',  ( -18.39999999999999858, 13.19494617735151465, -207.6708402378485516 ) ) ;
#134346=CARTESIAN_POINT ( 'NONE',  ( 15.07585980824112859, 13.06404166453376980, -216.7291753257208029 ) ) ;
#134474=ORIENTED_EDGE ( 'NONE', *, *, #201955, .F. ) ;
#134730=CARTESIAN_POINT ( 'NONE',  ( 20.99999999999999645, 12.21861431488691707, -211.2854491503459826 ) ) ;
#134854=CARTESIAN_POINT ( 'NONE',  ( 23.24999999999999645, 15.91777359887373500, -218.8720307647289474 ) ) ;
#135129=( GEOMETRIC_REPRESENTATION_CONTEXT ( 3 ) GLOBAL_UNCERTAINTY_ASSIGNED_CONTEXT ( ( #232894 ) ) GLOBAL_UNIT_ASSIGNED_CONTEXT ( ( #248402, #170201, #205399 ) ) REPRESENTATION_CONTEXT ( 'NONE', 'WORKASPACE' ) );
#135160=DIRECTION ( 'NONE',  ( 0.000000000000000000, 0.000000000000000000, 1.000000000000000000 ) ) ;
#135197=ADVANCED_FACE ( 'NONE', ( #111410 ), #4462, .T. ) ;
#135217=EDGE_CURVE ( 'NONE', #103352, #224045, #93111, .T. ) ;
#135256=ORIENTED_EDGE ( 'NONE', *, *, #78419, .F. ) ;
#135298=VERTEX_POINT ( 'NONE', #141243 ) ;
#135307=PLANE ( 'NONE',  #182991 ) ;
#135452=CARTESIAN_POINT ( 'NONE',  ( -16.82055514392383699, 12.41973608413271535, -211.2690732309943371 ) ) ;
#135524=CARTESIAN_POINT ( 'NONE',  ( -16.87331047859651179, 12.41403342719998726, -211.2428889513006993 ) ) ;
#135559=CARTESIAN_POINT ( 'NONE',  ( 20.27550659511088682, 10.97336462231075416, -208.0769506682813130 ) ) ;
#135638=CARTESIAN_POINT ( 'NONE',  ( 12.33938619321247288, 12.83074261044330022, -215.9253900757178428 ) ) ;
#135712=AXIS2_PLACEMENT_3D ( 'NONE', #180640, #22872, #59362 ) ;
#135793=CARTESIAN_POINT ( 'NONE',  ( -16.93970660449832621, 12.45464092817497814, -211.1340361583801268 ) ) ;
#136062=FACE_OUTER_BOUND ( 'NONE', #101449, .T. ) ;
#136070=LINE ( 'NONE', #115251, #171144 ) ;
#136113=( BOUNDED_CURVE ( )  B_SPLINE_CURVE ( 3, ( #104186, #106758, #122499, #85891 ),
 .UNSPECIFIED., .F., .F. ) 
 B_SPLINE_CURVE_WITH_KNOTS ( ( 4, 4 ),
 ( 1.570796326794908992, 2.617993877991470875 ),
 .UNSPECIFIED. ) 
 CURVE ( )  GEOMETRIC_REPRESENTATION_ITEM ( )  RATIONAL_B_SPLINE_CURVE ( ( 1.000000000000000000, 0.9106836025229650966, 0.9106836025229650966, 1.000000000000000000 ) ) 
 REPRESENTATION_ITEM ( '' )  );
#136222=DIRECTION ( 'NONE',  ( 1.000000000000000000, 0.000000000000000000, 0.000000000000000000 ) ) ;
#136439=ORIENTED_EDGE ( 'NONE', *, *, #108863, .F. ) ;
#136447=CARTESIAN_POINT ( 'NONE',  ( 12.47034474403011473, 12.53792204840291546, -214.5112614470119183 ) ) ;
#136791=CARTESIAN_POINT ( 'NONE',  ( -14.77738660682464022, 12.45029792656132095, -213.8222050902128331 ) ) ;
#137066=CARTESIAN_POINT ( 'NONE',  ( -16.80891096016305397, 14.16276025102163771, -219.2723308067244830 ) ) ;
#137372=CARTESIAN_POINT ( 'NONE',  ( -17.05016517656249420, 14.15417143192140514, -219.2328944449856465 ) ) ;
#137400=CARTESIAN_POINT ( 'NONE',  ( -16.78270389226385717, 14.15456323211786582, -219.2470401007283272 ) ) ;
#137598=CARTESIAN_POINT ( 'NONE',  ( -17.29158576265543346, 14.82658187305711373, -220.3713364495094709 ) ) ;
#137737=CARTESIAN_POINT ( 'NONE',  ( 15.70340296795548163, 12.60783650272741063, -214.9246183040210383 ) ) ;
#137983=ADVANCED_FACE ( 'NONE', ( #54253 ), #71287, .F. ) ;
#138047=CARTESIAN_POINT ( 'NONE',  ( -16.94445028196808778, 12.44605341304038859, -211.1922452800140775 ) ) ;
#138094=CARTESIAN_POINT ( 'NONE',  ( -17.01473183483382456, 12.43531352672262180, -211.3405985074572584 ) ) ;
#138105=CARTESIAN_POINT ( 'NONE',  ( -16.97683809663752186, 12.57413723904469904, -211.9780204941619104 ) ) ;
#138322=CARTESIAN_POINT ( 'NONE',  ( -16.79270642812277359, 14.15297681976097977, -219.2450585461133130 ) ) ;
#138560=CARTESIAN_POINT ( 'NONE',  ( -17.78043020864321377, 12.80471010483343619, -208.7905335770795716 ) ) ;
#138754=ORIENTED_EDGE ( 'NONE', *, *, #86774, .T. ) ;
#138794=ORIENTED_EDGE ( 'NONE', *, *, #71138, .T. ) ;
#138945=VECTOR ( 'NONE', #114756, 1000.000000000000227 ) ;
#138975=FACE_OUTER_BOUND ( 'NONE', #227624, .T. ) ;
#139026=DIRECTION ( 'NONE',  ( 0.000000000000000000, 0.2128009952263603677, -0.9770955615653313941 ) ) ;
#139060=DIRECTION ( 'NONE',  ( -1.000000000000000000, -2.283407518332345398E-16, 1.048447799332034305E-15 ) ) ;
#139062=EDGE_LOOP ( 'NONE', ( #31457, #199597, #235123, #171539, #148953 ) ) ;
#139285=CARTESIAN_POINT ( 'NONE',  ( 20.05000000000002913, 11.52084357182977570, -219.8296352432475942 ) ) ;
#139323=DIRECTION ( 'NONE',  ( 0.000000000000000000, 0.2128009952263605342, -0.9770955615653315052 ) ) ;
#139546=CARTESIAN_POINT ( 'NONE',  ( -16.97683809663752186, 11.69051004343035771, -207.9207640419785719 ) ) ;
#139605=CARTESIAN_POINT ( 'NONE',  ( -16.82542659449969591, 14.12371795089690352, -219.1659029699155781 ) ) ;
#139625=AXIS2_PLACEMENT_3D ( 'NONE', #26745, #121972, #183234 ) ;
#139651=LINE ( 'NONE', #60125, #112667 ) ;
#139720=VERTEX_POINT ( 'NONE', #31468 ) ;
#140013=( BOUNDED_SURFACE ( )  B_SPLINE_SURFACE ( 3, 2, ( 
 ( #5954, #185894, #24280 ),
 ( #165053, #3390, #242017 ),
 ( #25556, #63367, #47649 ),
 ( #206746, #187205, #142893 ) ),
 .UNSPECIFIED., .F., .F., .F. ) 
 B_SPLINE_SURFACE_WITH_KNOTS ( ( 4, 4 ),
 ( 3, 3 ),
 ( 0.3000847527772387280, 0.5552748953338751958 ),
 ( 0.000000000000000000, 1.000000000000000000 ),
 .UNSPECIFIED. ) 
 GEOMETRIC_REPRESENTATION_ITEM ( )  RATIONAL_B_SPLINE_SURFACE ( (
 ( 1.000000000000000000, 0.9152888060719439611, 1.000000000000000000),
 ( 1.000000000000000000, 0.9104333467450288486, 1.000000000000000000),
 ( 1.000000000000000000, 0.9035312726221058632, 1.000000000000000000),
 ( 1.000000000000000000, 0.8946697475932068322, 1.000000000000000000) ) ) 
 REPRESENTATION_ITEM ( '' )  SURFACE ( )  );
#140257=VECTOR ( 'NONE', #180611, 1000.000000000000114 ) ;
#140328=CARTESIAN_POINT ( 'NONE',  ( 16.87683809663749557, 14.15900158805613174, -219.2550725561364118 ) ) ;
#140335=ORIENTED_EDGE ( 'NONE', *, *, #231947, .F. ) ;
#140390=ADVANCED_FACE ( 'NONE', ( #88559 ), #247656, .T. ) ;
#140466=VECTOR ( 'NONE', #199571, 1000.000000000000227 ) ;
#140607=CARTESIAN_POINT ( 'NONE',  ( -16.78569801330232281, 12.41348556013404192, -211.2500832240831130 ) ) ;
#140621=CARTESIAN_POINT ( 'NONE',  ( 18.54999999999999716, 26.68086916408615750, -212.3318337774905160 ) ) ;
#140785=DIRECTION ( 'NONE',  ( 0.000000000000000000, 0.2128009952263605342, -0.9770955615653315052 ) ) ;
#140795=AXIS2_PLACEMENT_3D ( 'NONE', #23988, #66939, #4387 ) ;
#140837=ORIENTED_EDGE ( 'NONE', *, *, #39328, .F. ) ;
#140848=( BOUNDED_CURVE ( )  B_SPLINE_CURVE ( 3, ( #215851, #257507, #137598, #18947 ),
 .UNSPECIFIED., .F., .F. ) 
 B_SPLINE_CURVE_WITH_KNOTS ( ( 4, 4 ),
 ( 5.733388419619902088, 5.983100554402347449 ),
 .UNSPECIFIED. ) 
 CURVE ( )  GEOMETRIC_REPRESENTATION_ITEM ( )  RATIONAL_B_SPLINE_CURVE ( ( 1.000000000000000000, 0.9948104011409417691, 0.9948104011409417691, 1.000000000000000000 ) ) 
 REPRESENTATION_ITEM ( '' )  );
#140949=MECHANICAL_DESIGN_GEOMETRIC_PRESENTATION_REPRESENTATION('',(#253361),#91052);
#141081=CARTESIAN_POINT ( 'NONE',  ( -16.83199030136657370, 12.42117176568584824, -211.3666045650834633 ) ) ;
#141228=LINE ( 'NONE', #159520, #7910 ) ;
#141243=CARTESIAN_POINT ( 'NONE',  ( 15.74999999999999645, 13.18880795147152618, -215.2702608532411830 ) ) ;
#141353=ORIENTED_EDGE ( 'NONE', *, *, #48345, .F. ) ;
#141475=ORIENTED_EDGE ( 'NONE', *, *, #20926, .T. ) ;
#141668=ORIENTED_EDGE ( 'NONE', *, *, #247727, .F. ) ;
#141782=CARTESIAN_POINT ( 'NONE',  ( 18.39999999999999503, 8.212522512469059066, -212.1579332307740344 ) ) ;
#142180=ADVANCED_FACE ( 'NONE', ( #101096 ), #226054, .T. ) ;
#142199=CARTESIAN_POINT ( 'NONE',  ( -16.87683809663752754, 13.99889777621145903, -218.5199410132753428 ) ) ;
#142262=EDGE_LOOP ( 'NONE', ( #81383, #122230, #189936, #200922 ) ) ;
#142300=ORIENTED_EDGE ( 'NONE', *, *, #255720, .F. ) ;
#142348=CARTESIAN_POINT ( 'NONE',  ( -16.87372386987899020, 12.45246834913251455, -211.7454916664752886 ) ) ;
#142350=VECTOR ( 'NONE', #165209, 1000.000000000000227 ) ;
#142444=CARTESIAN_POINT ( 'NONE',  ( -16.89318236219976654, 12.41444193003837881, -211.2375501061338525 ) ) ;
#142560=VERTEX_POINT ( 'NONE', #168247 ) ;
#142817=CARTESIAN_POINT ( 'NONE',  ( -16.94878442675511820, 14.20790807310963899, -219.2835367392106889 ) ) ;
#142833=VECTOR ( 'NONE', #133303, 1000.000000000000000 ) ;
#142893=CARTESIAN_POINT ( 'NONE',  ( -18.37013991200266005, 16.40593182862863131, -222.2894472230003942 ) ) ;
#143045=VECTOR ( 'NONE', #257002, 1000.000000000000000 ) ;
#143421=ORIENTED_EDGE ( 'NONE', *, *, #244079, .F. ) ;
#143449=DIRECTION ( 'NONE',  ( -1.186688945009010077E-16, 0.9770955615653317272, 0.2128009952263595073 ) ) ;
#143802=EDGE_CURVE ( 'NONE', #251152, #171702, #250284, .T. ) ;
#143833=B_SPLINE_CURVE_WITH_KNOTS ( 'NONE', 3,
 ( #241466, #6693, #84915, #25005, #83626, #201046, #82347, #141081, #245318, #161942, #41996, #142348, #163217, #221865 ),
 .UNSPECIFIED., .F., .F.,
 ( 4, 2, 2, 2, 2, 2, 4 ),
 ( 0.000000000000000000, 2.389617747644273823E-05, 4.779235495288547647E-05, 9.558470990577095294E-05, 0.0001911694198115423396, 0.0003823388396230035808, 0.0007646776792460092216 ),
 .UNSPECIFIED. ) ;
#143842=EDGE_CURVE ( 'NONE', #125974, #231927, #221398, .T. ) ;
#143868=EDGE_CURVE ( 'NONE', #186535, #187411, #123614, .T. ) ;
#143896=LINE ( 'NONE', #241723, #162655 ) ;
#144106=ORIENTED_EDGE ( 'NONE', *, *, #70701, .F. ) ;
#144207=CARTESIAN_POINT ( 'NONE',  ( -16.94333152886235538, 12.44450707589361826, -211.1932353086754972 ) ) ;
#144273=CARTESIAN_POINT ( 'NONE',  ( -21.64999999999999858, 11.82777609026078025, -211.3705695484364924 ) ) ;
#144383=CARTESIAN_POINT ( 'NONE',  ( -16.79140778683509083, 14.14974710992871643, -219.2363503299867489 ) ) ;
#144413=EDGE_CURVE ( 'NONE', #175353, #103723, #151883, .T. ) ;
#144593=AXIS2_PLACEMENT_3D ( 'NONE', #187268, #4733, #125982 ) ;
#144598=ADVANCED_FACE ( 'NONE', ( #219513 ), #117849, .T. ) ;
#144652=VERTEX_POINT ( 'NONE', #166009 ) ;
#144752=CARTESIAN_POINT ( 'NONE',  ( -16.86337532320261090, 14.20933363574807728, -219.3453541648266309 ) ) ;
#144758=ORIENTED_EDGE ( 'NONE', *, *, #147647, .T. ) ;
#144816=ORIENTED_EDGE ( 'NONE', *, *, #167239, .T. ) ;
#145024=ORIENTED_EDGE ( 'NONE', *, *, #76129, .T. ) ;
#145147=CARTESIAN_POINT ( 'NONE',  ( -18.40000000000000213, 13.89349365668996228, -210.8782859590407668 ) ) ;
#145149=FACE_OUTER_BOUND ( 'NONE', #234873, .T. ) ;
#145201=VECTOR ( 'NONE', #208757, 1000.000000000000227 ) ;
#145316=CYLINDRICAL_SURFACE ( 'NONE', #105482, 1.749999999999998002 ) ;
#145635=AXIS2_PLACEMENT_3D ( 'NONE', #51582, #69925, #133717 ) ;
#145683=SURFACE_STYLE_USAGE ( .BOTH. , #66162 ) ;
#145888=CARTESIAN_POINT ( 'NONE',  ( -18.40000000000000213, 9.957490673325212427, -220.1701168356097469 ) ) ;
#146015=CARTESIAN_POINT ( 'NONE',  ( -18.40000000000000213, 16.37079970714667354, -222.2530670965321065 ) ) ;
#146080=ORIENTED_EDGE ( 'NONE', *, *, #205978, .T. ) ;
#146096=B_SPLINE_CURVE_WITH_KNOTS ( 'NONE', 3,
 ( #126172, #27124, #106600, #239727, #61073, #140607, #21968, #101437, #229149, #152199, #127473, #92186, #210863 ),
 .UNSPECIFIED., .F., .F.,
 ( 4, 3, 3, 3, 4 ),
 ( 1.110900444313928445E-16, 1.946463881814531607E-05, 3.922356109944008404E-05, 4.215060953238765177E-05, 4.415117091092261940E-05 ),
 .UNSPECIFIED. ) ;
#146205=ORIENTED_EDGE ( 'NONE', *, *, #55112, .F. ) ;
#146298=VERTEX_POINT ( 'NONE', #182731 ) ;
#146590=DIRECTION ( 'NONE',  ( -0.000000000000000000, 0.2128009952263603677, -0.9770955615653313941 ) ) ;
#146695=ORIENTED_EDGE ( 'NONE', *, *, #73552, .F. ) ;
#146824=DIRECTION ( 'NONE',  ( -1.000000000000000000, -1.631532756632575455E-14, -2.455126404641516337E-15 ) ) ;
#147037=B_SPLINE_CURVE_WITH_KNOTS ( 'NONE', 3,
 ( #205655, #11324, #206959, #10035, #166575, #27067, #106549, #67438, #25753, #128712, #89561, #144383, #208255, #204376 ),
 .UNSPECIFIED., .F., .F.,
 ( 4, 2, 2, 2, 2, 2, 4 ),
 ( 1.734723475976807094E-18, 0.0003823333598417674945, 0.0005735000397626501033, 0.0006690833797230904319, 0.0007168750497033101084, 0.0007407708846934187540, 0.0007646667196835271827 ),
 .UNSPECIFIED. ) ;
#147055=CARTESIAN_POINT ( 'NONE',  ( -12.25000000000000178, 12.70026017068886404, -215.3766613508543628 ) ) ;
#147162=CARTESIAN_POINT ( 'NONE',  ( -18.39999999999999858, 13.44928205424795564, -207.5377222505711075 ) ) ;
#147241=FACE_OUTER_BOUND ( 'NONE', #125845, .T. ) ;
#147259=EDGE_CURVE ( 'NONE', #214748, #233400, #136070, .T. ) ;
#147464=CARTESIAN_POINT ( 'NONE',  ( -16.86337532320262156, 12.42226302398836069, -211.1398532408442748 ) ) ;
#147513=CARTESIAN_POINT ( 'NONE',  ( 16.27683809663749770, 11.10425270649115959, -208.0484446391143649 ) ) ;
#147556=B_SPLINE_CURVE_WITH_KNOTS ( 'NONE', 3,
 ( #131786, #251737, #30144, #90078, #150095, #109644, #189204, #170970, #229613, #211332 ),
 .UNSPECIFIED., .F., .F.,
 ( 4, 3, 3, 4 ),
 ( 1.953413405799106337E-15, 8.145022132829330989E-06, 1.905645951092428095E-05, 2.061107371225752284E-05 ),
 .UNSPECIFIED. ) ;
#147647=EDGE_CURVE ( 'NONE', #69452, #139720, #173300, .T. ) ;
#147720=EDGE_CURVE ( 'NONE', #183798, #196416, #235476, .T. ) ;
#148055=EDGE_CURVE ( 'NONE', #169097, #220497, #102545, .T. ) ;
#148200=ORIENTED_EDGE ( 'NONE', *, *, #236304, .F. ) ;
#148476=CARTESIAN_POINT ( 'NONE',  ( 18.39999999999999503, 16.37079970714666999, -222.2530670965321065 ) ) ;
#148493=CARTESIAN_POINT ( 'NONE',  ( -15.66061380678751824, 12.83074261044330022, -215.9253900757177291 ) ) ;
#148623=VECTOR ( 'NONE', #64250, 1000.000000000000114 ) ;
#148953=ORIENTED_EDGE ( 'NONE', *, *, #231615, .F. ) ;
#149083=EDGE_LOOP ( 'NONE', ( #41409, #30036, #92754, #99497, #171829, #90091, #88071, #60728, #37458, #70724, #190732, #127951, #208758, #50401, #255347, #125821, #112753, #65644 ) ) ;
#149136=DIRECTION ( 'NONE',  ( -0.7071067811865456854, 0.6909108974501254608, 0.1504730267678059674 ) ) ;
#149274=VERTEX_POINT ( 'NONE', #71029 ) ;
#149575=( NAMED_UNIT ( * ) SI_UNIT ( $, .STERADIAN. ) SOLID_ANGLE_UNIT ( ) );
#149639=CARTESIAN_POINT ( 'NONE',  ( -16.88853107394619357, 14.16048480777639362, -219.2577547055215064 ) ) ;
#149822=DIRECTION ( 'NONE',  ( 0.000000000000000000, -0.2128009952263603677, 0.9770955615653313941 ) ) ;
#149859=DIRECTION ( 'NONE',  ( 1.186688945009010077E-16, -0.9770955615653315052, -0.2128009952263603954 ) ) ;
#149948=CARTESIAN_POINT ( 'NONE',  ( -18.34804628011471195, 13.17878477875115806, -207.5966336730521675 ) ) ;
#150057=CARTESIAN_POINT ( 'NONE',  ( -16.86578989773641624, 12.42364512751820982, -211.1234428391631752 ) ) ;
#150062=EDGE_CURVE ( 'NONE', #82079, #144652, #129126, .T. ) ;
#150095=CARTESIAN_POINT ( 'NONE',  ( -16.88219499860498019, 12.41408822593690964, -211.2421705250320088 ) ) ;
#150163=VECTOR ( 'NONE', #60226, 1000.000000000000227 ) ;
#150216=EDGE_CURVE ( 'NONE', #46719, #203112, #19747, .T. ) ;
#150621=CARTESIAN_POINT ( 'NONE',  ( 21.72449340488910252, 12.01681723992382622, -207.8496978137663689 ) ) ;
#150677=CARTESIAN_POINT ( 'NONE',  ( -18.40000000000000213, 15.66855642289968031, -219.0286517433665381 ) ) ;
#150863=ORIENTED_EDGE ( 'NONE', *, *, #221212, .F. ) ;
#150905=CARTESIAN_POINT ( 'NONE',  ( -18.40000000000000213, 16.37093090900293646, -222.2277664635145982 ) ) ;
#151014=EDGE_CURVE ( 'NONE', #171657, #91388, #240861, .T. ) ;
#151024=EDGE_CURVE ( 'NONE', #58136, #58804, #143833, .T. ) ;
#151107=CARTESIAN_POINT ( 'NONE',  ( -17.80356949363338259, 12.81667427061739950, -208.7367314240743497 ) ) ;
#151387=CARTESIAN_POINT ( 'NONE',  ( 12.68104795156994413, 12.99171346507298708, -216.4962224982961345 ) ) ;
#151468=EDGE_CURVE ( 'NONE', #233793, #58804, #70200, .T. ) ;
#151883=LINE ( 'NONE', #213103, #194780 ) ;
#152091=CARTESIAN_POINT ( 'NONE',  ( 20.27550659511089037, 13.44185616693653529, -219.4112591824391529 ) ) ;
#152163=DIRECTION ( 'NONE',  ( 0.000000000000000000, 0.2128009952263603677, -0.9770955615653313941 ) ) ;
#152199=CARTESIAN_POINT ( 'NONE',  ( -16.77828822508139694, 12.41303647063107718, -211.2560303524380174 ) ) ;
#152413=CARTESIAN_POINT ( 'NONE',  ( -16.87036670365549540, 12.42497885867826568, -211.1079079717509046 ) ) ;
#152683=CARTESIAN_POINT ( 'NONE',  ( 12.48201962039795987, 12.91318972656261188, -216.2290661304645596 ) ) ;
#152691=DIRECTION ( 'NONE',  ( 1.000000000000000000, 0.000000000000000000, 0.000000000000000000 ) ) ;
#153008=CARTESIAN_POINT ( 'NONE',  ( -15.55912972643740488, 12.75457250812873689, -219.6632863702431848 ) ) ;
#153053=( BOUNDED_CURVE ( )  B_SPLINE_CURVE ( 3, ( #115609, #195179, #232584, #76042 ),
 .UNSPECIFIED., .F., .F. ) 
 B_SPLINE_CURVE_WITH_KNOTS ( ( 4, 4 ),
 ( 2.589852378279006828, 2.850972632318391042 ),
 .UNSPECIFIED. ) 
 CURVE ( )  GEOMETRIC_REPRESENTATION_ITEM ( )  RATIONAL_B_SPLINE_CURVE ( ( 1.000000000000000000, 0.9943260843901261525, 0.9943260843901261525, 1.000000000000000000 ) ) 
 REPRESENTATION_ITEM ( '' )  );
#153303=AXIS2_PLACEMENT_3D ( 'NONE', #134730, #215564, #38233 ) ;
#153513=CARTESIAN_POINT ( 'NONE',  ( 0.000000000000000000, 0.000000000000000000, 0.000000000000000000 ) ) ;
#153620=ORIENTED_EDGE ( 'NONE', *, *, #20276, .F. ) ;
#153924=EDGE_CURVE ( 'NONE', #109830, #3891, #130260, .T. ) ;
#153984=CARTESIAN_POINT ( 'NONE',  ( 12.26145404764308111, 12.75065881068273654, -215.6014281960218852 ) ) ;
#154137=CARTESIAN_POINT ( 'NONE',  ( -16.93255653858138388, 12.44682876851034870, -211.1657874719333563 ) ) ;
#154266=AXIS2_PLACEMENT_3D ( 'NONE', #200988, #130430, #228265 ) ;
#154401=DIRECTION ( 'NONE',  ( 1.000000000000000000, -2.283407518332345398E-16, 1.048447799332034305E-15 ) ) ;
#154404=CARTESIAN_POINT ( 'NONE',  ( -16.94389599337535657, 14.20826918932317895, -219.2876906590868487 ) ) ;
#154674=CARTESIAN_POINT ( 'NONE',  ( -16.81744102076749314, 12.41403342719998726, -211.2428889513006993 ) ) ;
#154678=DIRECTION ( 'NONE',  ( -0.000000000000000000, 0.2128009952263603677, -0.9770955615653313941 ) ) ;
#154844=B_SPLINE_CURVE_WITH_KNOTS ( 'NONE', 3,
 ( #109189, #30990, #27140, #106613, #186185, #149639, #8828, #128781, #7538, #88326 ),
 .UNSPECIFIED., .F., .F.,
 ( 4, 3, 3, 4 ),
 ( 0.000000000000000000, 1.004626015990974373E-05, 1.831183478182685622E-05, 2.062343583996223352E-05 ),
 .UNSPECIFIED. ) ;
#154857=ORIENTED_EDGE ( 'NONE', *, *, #16129, .T. ) ;
#154875=CARTESIAN_POINT ( 'NONE',  ( -16.93234230245722216, 14.22041164560202375, -219.3109751335834687 ) ) ;
#155065=CARTESIAN_POINT ( 'NONE',  ( -16.84981964351492678, 12.42883166081041502, -211.4644154259821676 ) ) ;
#155341=PRODUCT_DEFINITION ( 'UNKNOWN', '', #82056, #14157 ) ;
#155346=DIRECTION ( 'NONE',  ( -0.000000000000000000, 0.2128009952263604232, -0.9770955615653316162 ) ) ;
#155387=ORIENTED_EDGE ( 'NONE', *, *, #43207, .F. ) ;
#155388=CARTESIAN_POINT ( 'NONE',  ( 16.87683809663750267, 12.41403342719998371, -211.2428889513006993 ) ) ;
#155526=AXIS2_PLACEMENT_3D ( 'NONE', #150621, #248440, #193603 ) ;
#155655=VERTEX_POINT ( 'NONE', #82015 ) ;
#155842=PLANE ( 'NONE',  #127612 ) ;
#155967=EDGE_CURVE ( 'NONE', #223991, #106564, #217382, .T. ) ;
#156350=CARTESIAN_POINT ( 'NONE',  ( -16.85697194749127803, 12.43417586606322445, -211.5301872951059750 ) ) ;
#156405=CARTESIAN_POINT ( 'NONE',  ( -13.88555196119802915, 12.43281162335558321, -213.6438014222476909 ) ) ;
#156457=CARTESIAN_POINT ( 'NONE',  ( 18.39999999999999503, 16.64129698264336099, -222.1941556740511032 ) ) ;
#156537=DIRECTION ( 'NONE',  ( -1.000000000000000000, 0.000000000000000000, 0.000000000000000000 ) ) ;
#156667=CARTESIAN_POINT ( 'NONE',  ( -16.83558968593873928, 14.15638303188477742, -219.2430492119315204 ) ) ;
#156693=CARTESIAN_POINT ( 'NONE',  ( -16.93339986808596720, 12.44999860098303657, -211.1490805700459248 ) ) ;
#156775=ADVANCED_FACE ( 'NONE', ( #238600, #61248, #200759 ), #122519, .T. ) ;
#156918=CARTESIAN_POINT ( 'NONE',  ( -17.11825945287482753, 12.43531352672262003, -211.3405985074572300 ) ) ;
#157173=CARTESIAN_POINT ( 'NONE',  ( -15.75000000000000355, 13.18880795147152440, -215.2702608532411830 ) ) ;
#157465=ORIENTED_EDGE ( 'NONE', *, *, #246825, .T. ) ;
#157663=EDGE_CURVE ( 'NONE', #113827, #101660, #106152, .T. ) ;
#157699=CARTESIAN_POINT ( 'NONE',  ( -15.06774609480955718, 12.47031117194349292, -214.0029172826438071 ) ) ;
#157966=CARTESIAN_POINT ( 'NONE',  ( -21.65000000000000213, 14.13772148853350430, -219.1573629999798811 ) ) ;
#158045=VECTOR ( 'NONE', #221594, 1000.000000000000227 ) ;
#158072=ORIENTED_EDGE ( 'NONE', *, *, #16144, .F. ) ;
#158166=ORIENTED_EDGE ( 'NONE', *, *, #15718, .F. ) ;
#158300=CARTESIAN_POINT ( 'NONE',  ( -16.80939487329394666, 14.15900158805632891, -219.2550725561372644 ) ) ;
#158359=( BOUNDED_CURVE ( )  B_SPLINE_CURVE ( 3, ( #135524, #173449, #138094, #115999 ),
 .UNSPECIFIED., .F., .F. ) 
 B_SPLINE_CURVE_WITH_KNOTS ( ( 4, 4 ),
 ( 0.5235987755983326775, 1.570796326794896558 ),
 .UNSPECIFIED. ) 
 CURVE ( )  GEOMETRIC_REPRESENTATION_ITEM ( )  RATIONAL_B_SPLINE_CURVE ( ( 1.000000000000000000, 0.9106836025229647635, 0.9106836025229647635, 1.000000000000000000 ) ) 
 REPRESENTATION_ITEM ( '' )  );
#158465=CARTESIAN_POINT ( 'NONE',  ( -18.40000000000000213, 8.212522512469059066, -212.1579332307740344 ) ) ;
#158569=ADVANCED_FACE ( 'NONE', ( #97589 ), #1395, .F. ) ;
#158863=UNCERTAINTY_MEASURE_WITH_UNIT (LENGTH_MEASURE( 1.000000000000000082E-05 ), #45316, 'distance_accuracy_value', 'NONE');
#158910=CARTESIAN_POINT ( 'NONE',  ( -21.65000000000000213, 14.25671114421267127, -219.2337924566137701 ) ) ;
#158965=CARTESIAN_POINT ( 'NONE',  ( -14.87779219673429054, 12.45596502558539243, -213.8760425650930870 ) ) ;
#159061=ORIENTED_EDGE ( 'NONE', *, *, #166495, .T. ) ;
#159219=CARTESIAN_POINT ( 'NONE',  ( -16.92280123533708647, 14.11630683194439051, -219.0590356125378548 ) ) ;
#159245=CARTESIAN_POINT ( 'NONE',  ( -16.93658211146646408, 12.44557776047770581, -211.1804511121877965 ) ) ;
#159520=CARTESIAN_POINT ( 'NONE',  ( -18.40000000000000213, 16.64129698264336099, -222.1941556740511032 ) ) ;
#160233=LINE ( 'NONE', #58511, #90962 ) ;
#160248=CARTESIAN_POINT ( 'NONE',  ( -13.22483237240078147, 12.45018385075468537, -213.8211107588515745 ) ) ;
#160350=CARTESIAN_POINT ( 'NONE',  ( -16.97683809663752186, 12.31632387104345305, -211.2641690508233125 ) ) ;
#160510=CARTESIAN_POINT ( 'NONE',  ( -16.88783316861813688, 14.13723969814692083, -219.1551508146100105 ) ) ;
#160596=CARTESIAN_POINT ( 'NONE',  ( 22.88900146558018989, 12.94144749016466456, -219.5202428567343702 ) ) ;
#160792=AXIS2_PLACEMENT_3D ( 'NONE', #256385, #59496, #139026 ) ;
#161560=EDGE_LOOP ( 'NONE', ( #43054, #38760, #70567, #199771, #178597 ) ) ;
#161608=VECTOR ( 'NONE', #25645, 1000.000000000000227 ) ;
#161851=DIRECTION ( 'NONE',  ( -0.7071067811865462405, 0.6909108974501249056, 0.1504730267678058564 ) ) ;
#161939=CARTESIAN_POINT ( 'NONE',  ( 23.24999999999999645, 14.17280543801757986, -210.8598471598932633 ) ) ;
#161942=CARTESIAN_POINT ( 'NONE',  ( -16.85312841634288361, 12.43107187334904395, -211.4921453644653866 ) ) ;
#162019=ORIENTED_EDGE ( 'NONE', *, *, #63237, .T. ) ;
#162111=CIRCLE ( 'NONE', #24553, 0.1000000000000054040 ) ;
#162202=( BOUNDED_CURVE ( )  B_SPLINE_CURVE ( 3, ( #110937, #11868, #173538, #253011 ),
 .UNSPECIFIED., .F., .T. ) 
 B_SPLINE_CURVE_WITH_KNOTS ( ( 4, 4 ),
 ( 5.731445031868799056, 5.983100554402348337 ),
 .UNSPECIFIED. ) 
 CURVE ( )  GEOMETRIC_REPRESENTATION_ITEM ( )  RATIONAL_B_SPLINE_CURVE ( ( 1.000000000000000000, 0.9947294176030464508, 0.9947294176030464508, 1.000000000000000000 ) ) 
 REPRESENTATION_ITEM ( '' )  );
#162289=CARTESIAN_POINT ( 'NONE',  ( 20.73486653747088582, 9.052352027204005225, -208.4953267290897259 ) ) ;
#162313=CARTESIAN_POINT ( 'NONE',  ( -18.40000000000000213, 14.17280543801757986, -210.8598471598932349 ) ) ;
#162317=CARTESIAN_POINT ( 'NONE',  ( -18.40000000000000213, 15.91777359887373500, -218.8720307647289758 ) ) ;
#162436=EDGE_CURVE ( 'NONE', #125974, #233400, #162111, .T. ) ;
#162531=CARTESIAN_POINT ( 'NONE',  ( -16.94445028196808778, 12.44605341304038859, -211.1922452800140775 ) ) ;
#162603=LINE ( 'NONE', #100015, #696 ) ;
#162655=VECTOR ( 'NONE', #63073, 1000.000000000000000 ) ;
#162744=CARTESIAN_POINT ( 'NONE',  ( -15.55912972643740488, 12.73329240860610234, -219.5655768140866542 ) ) ;
#162904=EDGE_CURVE ( 'NONE', #240326, #84962, #27315, .T. ) ;
#162984=AXIS2_PLACEMENT_3D ( 'NONE', #70185, #29785, #44189 ) ;
#163217=CARTESIAN_POINT ( 'NONE',  ( -16.87683809663753109, 12.46404896785209537, -211.8723793542922067 ) ) ;
#163534=CARTESIAN_POINT ( 'NONE',  ( 18.54999999999999716, 11.24151875332161765, -211.4982501455723138 ) ) ;
#163804=CARTESIAN_POINT ( 'NONE',  ( -16.90257928357875272, 12.41512770975328905, -211.2286145703175464 ) ) ;
#163910=CARTESIAN_POINT ( 'NONE',  ( -21.65000000000000213, 9.775875410973588586, -211.8174516384118817 ) ) ;
#165046=ORIENTED_EDGE ( 'NONE', *, *, #151014, .F. ) ;
#165053=CARTESIAN_POINT ( 'NONE',  ( -17.29838795458563183, 14.83790627693142383, -220.3913684649999709 ) ) ;
#165122=LINE ( 'NONE', #166439, #80217 ) ;
#165123=DIRECTION ( 'NONE',  ( 1.186688945009009831E-16, -0.9770955615653313941, -0.2128009952263603677 ) ) ;
#165209=DIRECTION ( 'NONE',  ( 0.000000000000000000, 0.9770955615653313941, 0.2128009952263603677 ) ) ;
#165362=ADVANCED_FACE ( 'NONE', ( #41845 ), #33420, .F. ) ;
#165385=PLANE ( 'NONE',  #96542 ) ;
#165399=VECTOR ( 'NONE', #42634, 1000.000000000000227 ) ;
#165494=CARTESIAN_POINT ( 'NONE',  ( -12.30589683808040924, 12.80332707393613134, -215.8182015632437185 ) ) ;
#165810=CARTESIAN_POINT ( 'NONE',  ( -16.98495255085917321, 14.21656675727647468, -219.2582788632799975 ) ) ;
#165967=ORIENTED_EDGE ( 'NONE', *, *, #97070, .T. ) ;
#166002=CARTESIAN_POINT ( 'NONE',  ( -16.87242674293850797, 12.41380142168690526, -211.2418236764092683 ) ) ;
#166009=CARTESIAN_POINT ( 'NONE',  ( -18.34374000495060386, 13.17878477875124688, -207.5966336730521391 ) ) ;
#166223=PLANE ( 'NONE',  #6910 ) ;
#166393=VERTEX_POINT ( 'NONE', #73317 ) ;
#166439=CARTESIAN_POINT ( 'NONE',  ( 18.39999999999999503, 9.957490673325212427, -220.1701168356097469 ) ) ;
#166495=EDGE_CURVE ( 'NONE', #91388, #32792, #241359, .T. ) ;
#166575=CARTESIAN_POINT ( 'NONE',  ( -16.85312964099708566, 14.07083882076682713, -219.0212948398784647 ) ) ;
#166691=ORIENTED_EDGE ( 'NONE', *, *, #120426, .T. ) ;
#166799=CARTESIAN_POINT ( 'NONE',  ( -15.57281606413133090, 12.88553809045803611, -216.1303193953969526 ) ) ;
#166944=CARTESIAN_POINT ( 'NONE',  ( -16.86733706339143879, 14.18592885272122217, -219.3035684813490320 ) ) ;
#166963=ORIENTED_EDGE ( 'NONE', *, *, #253966, .F. ) ;
#166969=EDGE_CURVE ( 'NONE', #119125, #202859, #53727, .T. ) ;
#167095=CARTESIAN_POINT ( 'NONE',  ( -17.11825945287482753, 12.53302308287915245, -211.3193184079345883 ) ) ;
#167188=CARTESIAN_POINT ( 'NONE',  ( -23.25000000000000355, 13.44928205424795564, -207.5377222505711075 ) ) ;
#167239=EDGE_CURVE ( 'NONE', #210898, #187411, #66887, .T. ) ;
#167344=VERTEX_POINT ( 'NONE', #257657 ) ;
#167526=DIRECTION ( 'NONE',  ( -1.000000000000000000, 0.000000000000000000, 0.000000000000000000 ) ) ;
#167625=CARTESIAN_POINT ( 'NONE',  ( -16.94225986326250677, 12.47717560563228822, -211.5328121362375953 ) ) ;
#167885=VECTOR ( 'NONE', #250873, 1000.000000000000000 ) ;
#168082=DIRECTION ( 'NONE',  ( -0.000000000000000000, 0.2128009952263604232, -0.9770955615653316162 ) ) ;
#168095=CARTESIAN_POINT ( 'NONE',  ( -14.11361717019516249, 13.17763673189382345, -217.0637590370182011 ) ) ;
#168247=CARTESIAN_POINT ( 'NONE',  ( -21.64999999999999858, 12.51174298335651791, -211.2216088517780292 ) ) ;
#168609=CARTESIAN_POINT ( 'NONE',  ( -20.65000000000000568, 9.775875410973588586, -211.8174516384118817 ) ) ;
#168611=DIRECTION ( 'NONE',  ( 0.000000000000000000, 0.2128009952263603677, -0.9770955615653313941 ) ) ;
#168624=AXIS2_PLACEMENT_3D ( 'NONE', #60968, #218749, #222590 ) ;
#168651=AXIS2_PLACEMENT_3D ( 'NONE', #73155, #75703, #152691 ) ;
#168682=B_SPLINE_CURVE_WITH_KNOTS ( 'NONE', 3,
 ( #255282, #20602, #16750, #177118, #240916, #100086, #235769, #179669, #976, #80515 ),
 .UNSPECIFIED., .F., .F.,
 ( 4, 2, 2, 2, 4 ),
 ( 5.262620404973387615E-16, 9.930191194504293527E-05, 0.0001986038238895596259, 0.0003972076477785142670, 0.0007944152955563421256 ),
 .UNSPECIFIED. ) ;
#168944=PLANE ( 'NONE',  #155526 ) ;
#169097=VERTEX_POINT ( 'NONE', #1053 ) ;
#169111=EDGE_CURVE ( 'NONE', #220350, #42401, #96313, .T. ) ;
#169179=VERTEX_POINT ( 'NONE', #139285 ) ;
#169195=EDGE_CURVE ( 'NONE', #100496, #125974, #66195, .T. ) ;
#169318=CARTESIAN_POINT ( 'NONE',  ( -16.93415306273742260, 14.21635907292751000, -219.3040454656228349 ) ) ;
#169340=ORIENTED_EDGE ( 'NONE', *, *, #73552, .T. ) ;
#169387=ORIENTED_EDGE ( 'NONE', *, *, #55112, .T. ) ;
#170004=EDGE_LOOP ( 'NONE', ( #55665, #96680, #192454, #178786 ) ) ;
#170013=CYLINDRICAL_SURFACE ( 'NONE', #205828, 0.1000000000000025868 ) ;
#170114=LINE ( 'NONE', #31868, #22141 ) ;
#170201=( NAMED_UNIT ( * ) PLANE_ANGLE_UNIT ( ) SI_UNIT ( $, .RADIAN. ) );
#170616=CARTESIAN_POINT ( 'NONE',  ( -16.94132844910802760, 14.21029813284434695, -219.2911855031067034 ) ) ;
#170622=EDGE_CURVE ( 'NONE', #224045, #180552, #228219, .T. ) ;
#170639=DIRECTION ( 'NONE',  ( 1.186688945009009831E-16, -0.9770955615653313941, -0.2128009952263603677 ) ) ;
#170970=CARTESIAN_POINT ( 'NONE',  ( -16.87435696428308063, 12.41403408133939301, -211.2428803809670512 ) ) ;
#171144=VECTOR ( 'NONE', #237768, 1000.000000000000000 ) ;
#171539=ORIENTED_EDGE ( 'NONE', *, *, #61842, .F. ) ;
#171657=VERTEX_POINT ( 'NONE', #243956 ) ;
#171702=VERTEX_POINT ( 'NONE', #50868 ) ;
#171728=DIRECTION ( 'NONE',  ( 1.000000000000000000, 0.000000000000000000, 0.000000000000000000 ) ) ;
#171829=ORIENTED_EDGE ( 'NONE', *, *, #117947, .T. ) ;
#171990=CARTESIAN_POINT ( 'NONE',  ( -17.73285935859659190, 12.78867406748397073, -208.6962744657041924 ) ) ;
#172232=CARTESIAN_POINT ( 'NONE',  ( -21.64999999999999858, 13.57274425111693539, -219.3827531532722048 ) ) ;
#172261=CARTESIAN_POINT ( 'NONE',  ( 13.88638282980483929, 13.17763673189382523, -217.0637590370182011 ) ) ;
#172454=FACE_OUTER_BOUND ( 'NONE', #38515, .T. ) ;
#172663=CARTESIAN_POINT ( 'NONE',  ( -18.38817693311004575, 16.37893853458640692, -222.2512945466943108 ) ) ;
#173176=EDGE_LOOP ( 'NONE', ( #29174, #122277, #166691, #244497 ) ) ;
#173178=CARTESIAN_POINT ( 'NONE',  ( -16.93353400591625757, 14.22995845551265681, -219.3242416127272065 ) ) ;
#173214=AXIS2_PLACEMENT_3D ( 'NONE', #53551, #32744, #156537 ) ;
#173300=LINE ( 'NONE', #254049, #127340 ) ;
#173449=CARTESIAN_POINT ( 'NONE',  ( -16.92507428761702215, 12.42752446970227176, -211.3048343277114895 ) ) ;
#173538=CARTESIAN_POINT ( 'NONE',  ( -17.22361732159832215, 12.52791994134343234, -209.9088836718198650 ) ) ;
#173928=ORIENTED_EDGE ( 'NONE', *, *, #75555, .F. ) ;
#174350=ORIENTED_EDGE ( 'NONE', *, *, #49919, .T. ) ;
#174638=EDGE_LOOP ( 'NONE', ( #78728, #60676, #83763, #218275 ) ) ;
#174778=CARTESIAN_POINT ( 'NONE',  ( -21.65000000000000213, 12.41403342719998548, -211.2428889513006993 ) ) ;
#174830=CARTESIAN_POINT ( 'NONE',  ( 15.73863059295127798, 12.75047551130876933, -215.6006359250795299 ) ) ;
#175209=CARTESIAN_POINT ( 'NONE',  ( -16.94107738177415712, 12.45552124806248706, -211.1315092113344463 ) ) ;
#175226=CARTESIAN_POINT ( 'NONE',  ( -18.38204789744325396, 16.37699364664935331, -222.2517181225500451 ) ) ;
#175284=ORIENTED_EDGE ( 'NONE', *, *, #35548, .T. ) ;
#175353=VERTEX_POINT ( 'NONE', #195314 ) ;
#175545=ORIENTED_EDGE ( 'NONE', *, *, #81848, .F. ) ;
#175619=CARTESIAN_POINT ( 'NONE',  ( 12.25000000000000355, 12.65163926562330410, -215.1534139431609560 ) ) ;
#175825=ORIENTED_EDGE ( 'NONE', *, *, #50527, .T. ) ;
#176092=ORIENTED_EDGE ( 'NONE', *, *, #59501, .F. ) ;
#176205=ORIENTED_EDGE ( 'NONE', *, *, #169195, .T. ) ;
#176245=CARTESIAN_POINT ( 'NONE',  ( -16.93440969289731157, 12.44567823802137241, -211.1758536839202804 ) ) ;
#176569=DIRECTION ( 'NONE',  ( -1.000000000000000000, 0.000000000000000000, 0.000000000000000000 ) ) ;
#176699=AXIS2_PLACEMENT_3D ( 'NONE', #92755, #155346, #234856 ) ;
#176913=CARTESIAN_POINT ( 'NONE',  ( 12.60053434924909688, 12.51008756600233340, -214.3176843001242275 ) ) ;
#177024=CARTESIAN_POINT ( 'NONE',  ( 21.72449340488910252, 12.74034062369345399, -211.1718227230884963 ) ) ;
#177046=FACE_OUTER_BOUND ( 'NONE', #83307, .T. ) ;
#177118=CARTESIAN_POINT ( 'NONE',  ( -16.89021194854739960, 14.13613997954251289, -219.1501013543562522 ) ) ;
#177196=CARTESIAN_POINT ( 'NONE',  ( -16.83558968593874994, 12.41665198337125098, -211.2549122955051359 ) ) ;
#177381=CARTESIAN_POINT ( 'NONE',  ( 13.12229106158773639, 13.10213769539062412, -216.8429874065679144 ) ) ;
#177517=CARTESIAN_POINT ( 'NONE',  ( -16.80621392010919735, 14.14295755150341627, -219.2180467217198725 ) ) ;
#177539=ORIENTED_EDGE ( 'NONE', *, *, #185193, .F. ) ;
#177827=CARTESIAN_POINT ( 'NONE',  ( -17.11825945287481687, 14.13772148853350252, -219.1573629999798527 ) ) ;
#178196=CARTESIAN_POINT ( 'NONE',  ( 13.22261339317536155, 12.45029792656131562, -213.8222050902127478 ) ) ;
#178216=CARTESIAN_POINT ( 'NONE',  ( 18.39999999999997371, 16.37079970714665933, -222.2530670965321349 ) ) ;
#178228=EDGE_CURVE ( 'NONE', #217875, #101660, #246253, .T. ) ;
#178252=EDGE_CURVE ( 'NONE', #84962, #88954, #49326, .T. ) ;
#178302=DIRECTION ( 'NONE',  ( 0.000000000000000000, 0.2128009952263603677, -0.9770955615653313941 ) ) ;
#178351=ORIENTED_EDGE ( 'NONE', *, *, #249232, .T. ) ;
#178476=CARTESIAN_POINT ( 'NONE',  ( -16.87683809663752754, 12.46323881132462397, -211.8640726678501380 ) ) ;
#178597=ORIENTED_EDGE ( 'NONE', *, *, #143868, .T. ) ;
#178627=EDGE_CURVE ( 'NONE', #149274, #182870, #256987, .T. ) ;
#178630=DIRECTION ( 'NONE',  ( 0.000000000000000000, 0.2128009952263604232, -0.9770955615653316162 ) ) ;
#178786=ORIENTED_EDGE ( 'NONE', *, *, #58664, .F. ) ;
#178803=CARTESIAN_POINT ( 'NONE',  ( -16.87333278164155104, 13.99033631766475416, -218.7973121421632641 ) ) ;
#179027=LINE ( 'NONE', #337, #242969 ) ;
#179206=APPLICATION_CONTEXT ( 'automotive_design' ) ;
#179382=ADVANCED_FACE ( 'NONE', ( #199807 ), #116408, .F. ) ;
#179567=VECTOR ( 'NONE', #252990, 1000.000000000000000 ) ;
#179669=CARTESIAN_POINT ( 'NONE',  ( -16.97048361161166952, 14.05449168777968261, -218.7752056288641427 ) ) ;
#179742=CARTESIAN_POINT ( 'NONE',  ( -16.93710578446436088, 12.47123518247324725, -211.5055361308018576 ) ) ;
#179914=DIRECTION ( 'NONE',  ( 0.000000000000000000, 0.9770955615653323934, 0.2128009952263564264 ) ) ;
#179982=EDGE_LOOP ( 'NONE', ( #83214, #166963, #155387, #186055 ) ) ;
#180174=ORIENTED_EDGE ( 'NONE', *, *, #183813, .F. ) ;
#180552=VERTEX_POINT ( 'NONE', #160596 ) ;
#180611=DIRECTION ( 'NONE',  ( 0.7071067811865462405, -0.6909108974501249056, -0.1504730267678058564 ) ) ;
#180640=CARTESIAN_POINT ( 'NONE',  ( -16.87036670365548474, 14.31214069770892472, -219.3240646258064430 ) ) ;
#180697=CARTESIAN_POINT ( 'NONE',  ( -16.94107738177414291, 14.24304960796391128, -219.3391119284832484 ) ) ;
#180790=CARTESIAN_POINT ( 'NONE',  ( 23.24999999999999645, 8.212522512469060842, -212.1579332307740344 ) ) ;
#181031=CARTESIAN_POINT ( 'NONE',  ( 18.39999999999999503, 13.78091005366907140, -222.8171174488881832 ) ) ;
#181263=EDGE_CURVE ( 'NONE', #101660, #139720, #143896, .T. ) ;
#181458=ORIENTED_EDGE ( 'NONE', *, *, #157663, .T. ) ;
#181502=DIRECTION ( 'NONE',  ( 1.000000000000000000, 0.000000000000000000, 0.000000000000000000 ) ) ;
#181596=CARTESIAN_POINT ( 'NONE',  ( -16.94878442675512531, 12.44667358478774055, -211.1966647789336093 ) ) ;
#181725=ORIENTED_EDGE ( 'NONE', *, *, #155967, .T. ) ;
#181978=CARTESIAN_POINT ( 'NONE',  ( -16.85718274719476995, 14.20298511439310296, -219.3341783597842038 ) ) ;
#182107=VECTOR ( 'NONE', #161851, 1000.000000000000114 ) ;
#182337=ORIENTED_EDGE ( 'NONE', *, *, #35548, .F. ) ;
#182433=AXIS2_PLACEMENT_3D ( 'NONE', #167095, #181502, #204882 ) ;
#182601=AXIS2_PLACEMENT_3D ( 'NONE', #147513, #8017, #48401 ) ;
#182610=VERTEX_POINT ( 'NONE', #7330 ) ;
#182731=CARTESIAN_POINT ( 'NONE',  ( -16.89268316805466341, 12.41449167011727361, -211.2369018264743090 ) ) ;
#182870=VERTEX_POINT ( 'NONE', #163534 ) ;
#182978=CARTESIAN_POINT ( 'NONE',  ( -16.77732147262506146, 14.15218621894316087, -219.2427314506515756 ) ) ;
#182991=AXIS2_PLACEMENT_3D ( 'NONE', #54499, #237001, #197857 ) ;
#183234=DIRECTION ( 'NONE',  ( 1.000000000000000000, 0.000000000000000000, 0.000000000000000000 ) ) ;
#183336=VECTOR ( 'NONE', #124375, 1000.000000000000227 ) ;
#183351=CIRCLE ( 'NONE', #220760, 1.749999999999999778 ) ;
#183441=LINE ( 'NONE', #144273, #165399 ) ;
#183460=VERTEX_POINT ( 'NONE', #155388 ) ;
#183763=CARTESIAN_POINT ( 'NONE',  ( -15.73854595235691534, 12.75065881068273832, -215.6014281960218852 ) ) ;
#183798=VERTEX_POINT ( 'NONE', #127791 ) ;
#183813=EDGE_CURVE ( 'NONE', #200838, #220497, #105956, .T. ) ;
#184158=ORIENTED_EDGE ( 'NONE', *, *, #244079, .T. ) ;
#184184=CARTESIAN_POINT ( 'NONE',  ( -16.94165728009538086, 14.20474050515682940, -219.2871285009821634 ) ) ;
#184286=CYLINDRICAL_SURFACE ( 'NONE', #20298, 0.1000000000000054040 ) ;
#184404=DIRECTION ( 'NONE',  ( 1.000000000000000000, -2.283407518332345398E-16, 1.048447799332034305E-15 ) ) ;
#184433=EDGE_CURVE ( 'NONE', #55301, #212340, #251906, .T. ) ;
#184735=LINE ( 'NONE', #163910, #200010 ) ;
#184763=DIRECTION ( 'NONE',  ( 0.000000000000000000, -0.9770955615653551529, -0.2128009952262517601 ) ) ;
#184815=DIRECTION ( 'NONE',  ( 1.073024830501117725E-15, -0.2128009952263604232, 0.9770955615653316162 ) ) ;
#184977=AXIS2_PLACEMENT_3D ( 'NONE', #25498, #102418, #204111 ) ;
#185193=EDGE_CURVE ( 'NONE', #182870, #46719, #20733, .T. ) ;
#185307=ORIENTED_EDGE ( 'NONE', *, *, #178627, .F. ) ;
#185350=CARTESIAN_POINT ( 'NONE',  ( -20.65000000000000568, 7.488999128699433072, -208.8358083214519070 ) ) ;
#185414=CARTESIAN_POINT ( 'NONE',  ( 18.39999999999997371, 13.44928205424795564, -207.5377222505711075 ) ) ;
#185519=EDGE_CURVE ( 'NONE', #100496, #15616, #54394, .T. ) ;
#185620=ORIENTED_EDGE ( 'NONE', *, *, #39212, .F. ) ;
#185722=DIRECTION ( 'NONE',  ( -1.020425574104003999E-15, 0.2128009952263603677, -0.9770955615653313941 ) ) ;
#185803=ORIENTED_EDGE ( 'NONE', *, *, #202271, .T. ) ;
#185894=CARTESIAN_POINT ( 'NONE',  ( -16.91256925476569251, 14.21894878281401375, -219.3624168839846789 ) ) ;
#186055=ORIENTED_EDGE ( 'NONE', *, *, #204351, .F. ) ;
#186185=CARTESIAN_POINT ( 'NONE',  ( -16.88593481969334675, 14.15994726773271850, -219.2567827423596043 ) ) ;
#186338=CARTESIAN_POINT ( 'NONE',  ( -15.39126916658603150, 12.96612044530440500, -216.4114274690425361 ) ) ;
#186361=ORIENTED_EDGE ( 'NONE', *, *, #241662, .T. ) ;
#186535=VERTEX_POINT ( 'NONE', #156457 ) ;
#186559=ORIENTED_EDGE ( 'NONE', *, *, #196340, .F. ) ;
#186820=AXIS2_PLACEMENT_3D ( 'NONE', #89779, #104204, #226725 ) ;
#186882=CARTESIAN_POINT ( 'NONE',  ( -18.40000000000000213, 13.84507122969784554, -210.9312241760660243 ) ) ;
#187205=CARTESIAN_POINT ( 'NONE',  ( -18.41431012584569515, 16.38972671430905947, -222.2727256927804262 ) ) ;
#187268=CARTESIAN_POINT ( 'NONE',  ( 20.04999999999999716, 11.24151875332161765, -211.4982501455723138 ) ) ;
#187271=DIRECTION ( 'NONE',  ( 0.000000000000000000, 0.9770955615653313941, 0.2128009952263603677 ) ) ;
#187406=PRESENTATION_STYLE_ASSIGNMENT (( #145683 ) ) ;
#187411=VERTEX_POINT ( 'NONE', #235055 ) ;
#187629=CARTESIAN_POINT ( 'NONE',  ( -14.56336952470180179, 13.14811317477304442, -216.9788617421937431 ) ) ;
#187749=ORIENTED_EDGE ( 'NONE', *, *, #144413, .T. ) ;
#188042=ORIENTED_EDGE ( 'NONE', *, *, #223125, .F. ) ;
#188318=DIRECTION ( 'NONE',  ( 1.000000000000000000, 1.159508501126949537E-16, 2.525285885220369759E-17 ) ) ;
#188761=ORIENTED_EDGE ( 'NONE', *, *, #28842, .T. ) ;
#188835=CARTESIAN_POINT ( 'NONE',  ( -16.93860193097148326, 14.21179149064447422, -219.2948891565064002 ) ) ;
#189056=CARTESIAN_POINT ( 'NONE',  ( -18.38639463286148867, 13.18566125533467215, -207.5951360497712699 ) ) ;
#189204=CARTESIAN_POINT ( 'NONE',  ( -16.87487986503753845, 12.41403543382080343, -211.2428626618309693 ) ) ;
#189534=CARTESIAN_POINT ( 'NONE',  ( 23.04999999999999716, 13.78091005366907140, -222.8171174488881832 ) ) ;
#189577=ORIENTED_EDGE ( 'NONE', *, *, #150062, .F. ) ;
#189702=ORIENTED_EDGE ( 'NONE', *, *, #61842, .T. ) ;
#189923=CIRCLE ( 'NONE', #65583, 0.9000000000000014655 ) ;
#189936=ORIENTED_EDGE ( 'NONE', *, *, #162436, .T. ) ;
#190037=CARTESIAN_POINT ( 'NONE',  ( -18.40000000000000213, 16.36019599348126619, -222.2043791590202488 ) ) ;
#190086=VERTEX_POINT ( 'NONE', #11947 ) ;
#190176=DIRECTION ( 'NONE',  ( 1.000000000000000000, 0.000000000000000000, 0.000000000000000000 ) ) ;
#190315=VERTEX_POINT ( 'NONE', #100419 ) ;
#190369=CYLINDRICAL_SURFACE ( 'NONE', #94451, 1.749999999999999778 ) ;
#190549=ORIENTED_EDGE ( 'NONE', *, *, #169111, .F. ) ;
#190732=ORIENTED_EDGE ( 'NONE', *, *, #73648, .T. ) ;
#190736=ADVANCED_FACE ( 'NONE', ( #239655 ), #2298, .F. ) ;
#191106=CARTESIAN_POINT ( 'NONE',  ( -18.40000000000000213, 15.50909414388701890, -218.9610367925635330 ) ) ;
#191218=ADVANCED_BREP_SHAPE_REPRESENTATION ( '', ( #20981, #2425 ), #135129 ) ;
#191559=VECTOR ( 'NONE', #25048, 1000.000000000000114 ) ;
#191658=ORIENTED_EDGE ( 'NONE', *, *, #121053, .T. ) ;
#191693=LINE ( 'NONE', #226926, #90488 ) ;
#191766=EDGE_LOOP ( 'NONE', ( #226294, #232869 ) ) ;
#191832=B_SPLINE_CURVE_WITH_KNOTS ( 'NONE', 3,
 ( #132730, #212269, #133990, #33668, #173178, #210972, #113150, #75340, #154875, #229263, #169318, #55697, #29805, #188835, #170616, #15353 ),
 .UNSPECIFIED., .F., .F.,
 ( 4, 3, 3, 3, 3, 4 ),
 ( 0.000000000000000000, 1.810570668010099324E-05, 2.740575833572219257E-05, 4.256816319435903717E-05, 5.213463471026593917E-05, 6.641585710720939166E-05 ),
 .UNSPECIFIED. ) ;
#192318=VECTOR ( 'NONE', #74404, 1000.000000000000227 ) ;
#192454=ORIENTED_EDGE ( 'NONE', *, *, #64115, .F. ) ;
#192519=VECTOR ( 'NONE', #71433, 1000.000000000000227 ) ;
#192817=EDGE_CURVE ( 'NONE', #220350, #117708, #36168, .T. ) ;
#192864=DIRECTION ( 'NONE',  ( 0.000000000000000000, -0.2128009952263603677, 0.9770955615653313941 ) ) ;
#192997=DIRECTION ( 'NONE',  ( 1.186688945009009831E-16, -0.9770955615653316162, -0.2128009952263604232 ) ) ;
#193073=CARTESIAN_POINT ( 'NONE',  ( 12.84435279558019261, 13.04030727965138503, -216.6527351471937095 ) ) ;
#193089=CIRCLE ( 'NONE', #88814, 0.5000000000000004441 ) ;
#193394=EDGE_CURVE ( 'NONE', #149274, #169179, #243015, .T. ) ;
#193603=DIRECTION ( 'NONE',  ( -0.5932847527679298016, 0.7865547670005542669, 0.1713032417725954826 ) ) ;
#193775=ORIENTED_EDGE ( 'NONE', *, *, #192817, .F. ) ;
#193781=DIRECTION ( 'NONE',  ( 0.000000000000000000, -0.2128009952263603677, 0.9770955615653313941 ) ) ;
#193897=CARTESIAN_POINT ( 'NONE',  ( 15.06592377766031099, 12.47014700295942369, -214.0015173037735394 ) ) ;
#194193=ORIENTED_EDGE ( 'NONE', *, *, #11514, .F. ) ;
#194379=PLANE ( 'NONE',  #168651 ) ;
#194508=CARTESIAN_POINT ( 'NONE',  ( 20.99999999999999645, 13.96358247574307221, -219.2976327551816951 ) ) ;
#194780=VECTOR ( 'NONE', #129719, 1000.000000000000227 ) ;
#194784=ORIENTED_EDGE ( 'NONE', *, *, #220856, .T. ) ;
#194982=CIRCLE ( 'NONE', #153303, 0.9000000000000014655 ) ;
#195179=CARTESIAN_POINT ( 'NONE',  ( 17.74533788810829904, 12.76545729867106971, -208.7752074168712397 ) ) ;
#195196=CARTESIAN_POINT ( 'NONE',  ( 13.12220780326571656, 12.45596502558539065, -213.8760425650930301 ) ) ;
#195314=CARTESIAN_POINT ( 'NONE',  ( 23.24999999999999645, 11.31241850904329205, -211.4828089347303433 ) ) ;
#195609=( BOUNDED_SURFACE ( )  B_SPLINE_SURFACE ( 3, 2, ( 
 ( #11605, #10324, #88533 ),
 ( #151107, #226778, #171990 ),
 ( #230646, #51979, #126395 ),
 ( #251472, #72882, #152413 ) ),
 .UNSPECIFIED., .F., .F., .F. ) 
 B_SPLINE_SURFACE_WITH_KNOTS ( ( 4, 4 ),
 ( 3, 3 ),
 ( 5.727910411845712702, 5.983100554402348337 ),
 ( 0.000000000000000000, 1.000000000000000000 ),
 .UNSPECIFIED. ) 
 GEOMETRIC_REPRESENTATION_ITEM ( )  RATIONAL_B_SPLINE_SURFACE ( (
 ( 1.000000000000000000, 0.8946697475932048338, 1.000000000000000000),
 ( 1.000000000000000000, 0.9035312726220381396, 1.000000000000000000),
 ( 1.000000000000000000, 0.9104333467450170803, 1.000000000000000000),
 ( 1.000000000000000000, 0.9152888060719308605, 1.000000000000000000) ) ) 
 REPRESENTATION_ITEM ( '' )  SURFACE ( )  );
#195650=CARTESIAN_POINT ( 'NONE',  ( 15.74999999999999645, 12.72489043187540148, -215.4897534858791630 ) ) ;
#196065=DIRECTION ( 'NONE',  ( -1.000000000000000000, 0.000000000000000000, 0.000000000000000000 ) ) ;
#196340=EDGE_CURVE ( 'NONE', #209959, #233793, #197724, .T. ) ;
#196416=VERTEX_POINT ( 'NONE', #157173 ) ;
#196438=CARTESIAN_POINT ( 'NONE',  ( 15.39793903038207112, 12.50981721680830105, -214.3157313002988928 ) ) ;
#196546=DIRECTION ( 'NONE',  ( -0.5932847527679298016, 0.7865547670005540448, 0.1713032417725961210 ) ) ;
#196717=CARTESIAN_POINT ( 'NONE',  ( -16.87683809663750623, 12.57413723904470082, -211.9780204941619104 ) ) ;
#196777=CARTESIAN_POINT ( 'NONE',  ( -18.39999999999999858, 13.18938849241619593, -207.6453216105643946 ) ) ;
#196988=ORIENTED_EDGE ( 'NONE', *, *, #28915, .F. ) ;
#197041=AXIS2_PLACEMENT_3D ( 'NONE', #55508, #52972, #193781 ) ;
#197067=CARTESIAN_POINT ( 'NONE',  ( -21.65000000000000213, 12.43531352672262003, -211.3405985074572300 ) ) ;
#197334=DIRECTION ( 'NONE',  ( 0.000000000000000000, 0.2128009952263603677, -0.9770955615653313941 ) ) ;
#197336=DIRECTION ( 'NONE',  ( 0.000000000000000000, -0.2128009952263603677, 0.9770955615653313941 ) ) ;
#197724=CIRCLE ( 'NONE', #102031, 0.09999999999999939493 ) ;
#197857=DIRECTION ( 'NONE',  ( -1.000000000000000000, -2.283407518332345398E-16, 1.048447799332034305E-15 ) ) ;
#198562=FACE_OUTER_BOUND ( 'NONE', #179982, .T. ) ;
#198657=DIRECTION ( 'NONE',  ( 0.000000000000000000, 0.9770955615653313941, 0.2128009952263603677 ) ) ;
#198852=LINE ( 'NONE', #162317, #25874 ) ;
#199070=CARTESIAN_POINT ( 'NONE',  ( -16.92132318717937522, 12.42386347980771077, -211.2125078751872707 ) ) ;
#199073=ORIENTED_EDGE ( 'NONE', *, *, #35413, .T. ) ;
#199170=EDGE_LOOP ( 'NONE', ( #134474, #228686, #40345, #95381 ) ) ;
#199191=LINE ( 'NONE', #120959, #246063 ) ;
#199248=ORIENTED_EDGE ( 'NONE', *, *, #147647, .F. ) ;
#199305=CARTESIAN_POINT ( 'NONE',  ( -16.87401514999228169, 12.42892566803711318, -211.3112680601871318 ) ) ;
#199314=ORIENTED_EDGE ( 'NONE', *, *, #208091, .F. ) ;
#199360=CARTESIAN_POINT ( 'NONE',  ( -13.54795643572457919, 12.43804190223351114, -213.6995959073539666 ) ) ;
#199571=DIRECTION ( 'NONE',  ( -0.000000000000000000, -0.2128009952263603677, 0.9770955615653313941 ) ) ;
#199597=ORIENTED_EDGE ( 'NONE', *, *, #71165, .F. ) ;
#199603=DIRECTION ( 'NONE',  ( -1.000000000000000000, 0.000000000000000000, 0.000000000000000000 ) ) ;
#199771=ORIENTED_EDGE ( 'NONE', *, *, #53249, .F. ) ;
#199807=FACE_OUTER_BOUND ( 'NONE', #42489, .T. ) ;
#199979=DIRECTION ( 'NONE',  ( 0.000000000000000000, -0.2128009952263403282, 0.9770955615653358350 ) ) ;
#200010=VECTOR ( 'NONE', #203020, 1000.000000000000000 ) ;
#200136=FACE_OUTER_BOUND ( 'NONE', #65069, .T. ) ;
#200499=DIRECTION ( 'NONE',  ( -1.073024830501117725E-15, -0.2128009952263604232, 0.9770955615653316162 ) ) ;
#200558=ORIENTED_EDGE ( 'NONE', *, *, #192817, .T. ) ;
#200744=DIRECTION ( 'NONE',  ( -1.000000000000000000, -1.159508501126949537E-16, -2.525285885220370376E-17 ) ) ;
#200759=FACE_BOUND ( 'NONE', #128857, .T. ) ;
#200838=VERTEX_POINT ( 'NONE', #105174 ) ;
#200922=ORIENTED_EDGE ( 'NONE', *, *, #147259, .F. ) ;
#200988=CARTESIAN_POINT ( 'NONE',  ( 20.99999999999999645, 11.49509093111729108, -207.9633242410238552 ) ) ;
#201046=CARTESIAN_POINT ( 'NONE',  ( -16.81453046979148880, 12.41652078041931873, -211.3055207088991665 ) ) ;
#201257=AXIS2_PLACEMENT_3D ( 'NONE', #218183, #117820, #252183 ) ;
#201776=VECTOR ( 'NONE', #185722, 1000.000000000000227 ) ;
#201914=CARTESIAN_POINT ( 'NONE',  ( -15.15766958671844300, 12.47908687115373105, -214.0766389635195139 ) ) ;
#201944=CARTESIAN_POINT ( 'NONE',  ( -20.65000000000000568, 9.052352027203962592, -208.4953267290897543 ) ) ;
#201955=EDGE_CURVE ( 'NONE', #182870, #190086, #160233, .T. ) ;
#202081=EDGE_LOOP ( 'NONE', ( #188761, #108053, #158166 ) ) ;
#202183=CARTESIAN_POINT ( 'NONE',  ( -16.86420534634261514, 14.19368693413156635, -219.3174569077499996 ) ) ;
#202271=EDGE_CURVE ( 'NONE', #233837, #166393, #92082, .T. ) ;
#202311=ORIENTED_EDGE ( 'NONE', *, *, #166969, .T. ) ;
#202507=CARTESIAN_POINT ( 'NONE',  ( 18.39999999999999503, 14.17280543801757986, -210.8598471598932349 ) ) ;
#202772=ORIENTED_EDGE ( 'NONE', *, *, #236076, .T. ) ;
#202859=VERTEX_POINT ( 'NONE', #206414 ) ;
#202885=AXIS2_PLACEMENT_3D ( 'NONE', #140621, #121102, #139323 ) ;
#203020=DIRECTION ( 'NONE',  ( 1.000000000000000000, 0.000000000000000000, 0.000000000000000000 ) ) ;
#203112=VERTEX_POINT ( 'NONE', #4057 ) ;
#203189=CARTESIAN_POINT ( 'NONE',  ( -12.93407622233968191, 12.47014700295942369, -214.0015173037735678 ) ) ;
#203228=EDGE_LOOP ( 'NONE', ( #254161, #3665, #90799, #238968 ) ) ;
#203327=CARTESIAN_POINT ( 'NONE',  ( -15.31895204843005942, 12.99171346507298530, -216.4962224982960777 ) ) ;
#203524=CARTESIAN_POINT ( 'NONE',  ( -15.55912972643741199, 10.98832424774994365, -211.5533932092509417 ) ) ;
#203648=AXIS2_PLACEMENT_3D ( 'NONE', #33708, #168082, #70254 ) ;
#203687=CARTESIAN_POINT ( 'NONE',  ( -23.25000000000000355, 9.957490673325212427, -220.1701168356097469 ) ) ;
#203824=VECTOR ( 'NONE', #18458, 1000.000000000000227 ) ;
#203850=DIRECTION ( 'NONE',  ( 0.000000000000000000, 0.2128009952263403282, -0.9770955615653358350 ) ) ;
#203970=CARTESIAN_POINT ( 'NONE',  ( 18.39999999999999503, 9.957490673325212427, -220.1701168356097469 ) ) ;
#204111=DIRECTION ( 'NONE',  ( 1.000000000000000000, 0.000000000000000000, 0.000000000000000000 ) ) ;
#204142=CARTESIAN_POINT ( 'NONE',  ( -16.89020380669786903, 12.43689062641632326, -211.3478399073821947 ) ) ;
#204218=CIRCLE ( 'NONE', #121051, 0.5000000000000004441 ) ;
#204261=LINE ( 'NONE', #90420, #161608 ) ;
#204330=CARTESIAN_POINT ( 'NONE',  ( 20.09999999999999787, 13.96358247574307043, -219.2976327551816951 ) ) ;
#204351=EDGE_CURVE ( 'NONE', #112987, #146298, #60164, .T. ) ;
#204376=CARTESIAN_POINT ( 'NONE',  ( -16.77683809663752257, 14.15196434607590348, -219.2423291894720307 ) ) ;
#204487=DIRECTION ( 'NONE',  ( -1.000000000000000000, 0.000000000000000000, 0.000000000000000000 ) ) ;
#204567=CARTESIAN_POINT ( 'NONE',  ( -18.40000000000000213, 8.212522512469059066, -212.1579332307740344 ) ) ;
#204594=CARTESIAN_POINT ( 'NONE',  ( -15.51798037960204368, 12.91318972656261188, -216.2290661304645880 ) ) ;
#204749=VERTEX_POINT ( 'NONE', #49340 ) ;
#204882=DIRECTION ( 'NONE',  ( 0.000000000000000000, 0.2128009952263403282, -0.9770955615653358350 ) ) ;
#205105=EDGE_CURVE ( 'NONE', #58804, #233793, #120901, .T. ) ;
#205240=CARTESIAN_POINT ( 'NONE',  ( -18.40000000000000213, 13.19198836721619017, -207.5937580722650466 ) ) ;
#205330=DIRECTION ( 'NONE',  ( 0.7071067811865463515, -0.6909108974501249056, -0.1504730267678058564 ) ) ;
#205399=( NAMED_UNIT ( * ) SI_UNIT ( $, .STERADIAN. ) SOLID_ANGLE_UNIT ( ) );
#205524=VERTEX_POINT ( 'NONE', #3138 ) ;
#205655=CARTESIAN_POINT ( 'NONE',  ( -16.87683809663752399, 13.90118822005493371, -218.5412211127979845 ) ) ;
#205785=CARTESIAN_POINT ( 'NONE',  ( 21.72449340488910252, 12.74034062369345399, -211.1718227230884963 ) ) ;
#205828=AXIS2_PLACEMENT_3D ( 'NONE', #153008, #149136, #232533 ) ;
#205882=CARTESIAN_POINT ( 'NONE',  ( -15.15564720441981095, 13.04030727965138503, -216.6527351471937664 ) ) ;
#205978=EDGE_CURVE ( 'NONE', #96084, #125974, #95779, .T. ) ;
#206002=ADVANCED_FACE ( 'NONE', ( #125384 ), #44563, .F. ) ;
#206414=CARTESIAN_POINT ( 'NONE',  ( -12.25000000000000178, 12.70026017068886404, -215.3766613508543628 ) ) ;
#206746=CARTESIAN_POINT ( 'NONE',  ( -18.44085059012131822, 16.40865159970219267, -222.2349014206415916 ) ) ;
#206816=CARTESIAN_POINT ( 'NONE',  ( 15.74999999999999645, 13.18880795147152618, -215.2702608532411830 ) ) ;
#206959=CARTESIAN_POINT ( 'NONE',  ( -16.87372397896795917, 13.98494438218169655, -218.7820011785657925 ) ) ;
#207189=CARTESIAN_POINT ( 'NONE',  ( -14.45422546970484312, 13.15902077901803224, -217.0103513519800060 ) ) ;
#207591=PRODUCT_DEFINITION_SHAPE ( 'NONE', 'NONE',  #155341 ) ;
#207655=CARTESIAN_POINT ( 'NONE',  ( -16.91256925476569606, 14.21894878281401198, -219.3624168839846789 ) ) ;
#207699=EDGE_CURVE ( 'NONE', #231927, #214748, #42857, .T. ) ;
#208022=ORIENTED_EDGE ( 'NONE', *, *, #207699, .T. ) ;
#208031=CARTESIAN_POINT ( 'NONE',  ( -16.81744102076749314, 12.41403342719998726, -211.2428889513006993 ) ) ;
#208091=EDGE_CURVE ( 'NONE', #139720, #171702, #218432, .T. ) ;
#208255=CARTESIAN_POINT ( 'NONE',  ( -16.78493211734303259, 14.15196434607596387, -219.2423291894721729 ) ) ;
#208323=VERTEX_POINT ( 'NONE', #238679 ) ;
#208481=CARTESIAN_POINT ( 'NONE',  ( -15.69373346032659455, 12.80368220771249632, -215.8196253896158794 ) ) ;
#208635=CARTESIAN_POINT ( 'NONE',  ( -18.40000000000000213, 13.19198836721619017, -207.5937580722650466 ) ) ;
#208757=DIRECTION ( 'NONE',  ( 1.652117596168391306E-15, 0.9770955615653313941, 0.2128009952263603677 ) ) ;
#208758=ORIENTED_EDGE ( 'NONE', *, *, #108863, .T. ) ;
#209021=AXIS2_PLACEMENT_3D ( 'NONE', #158465, #219680, #220963 ) ;
#209692=VERTEX_POINT ( 'NONE', #118885 ) ;
#209818=DIRECTION ( 'NONE',  ( 0.000000000000000000, 0.9770955615653313941, 0.2128009952263603677 ) ) ;
#209959=VERTEX_POINT ( 'NONE', #212547 ) ;
#209997=TOROIDAL_SURFACE ( 'NONE', #22547, 14.20833333333334103, 0.1000000000000000056 ) ;
#210008=PLANE ( 'NONE',  #84114 ) ;
#210119=VERTEX_POINT ( 'NONE', #138105 ) ;
#210530=AXIS2_PLACEMENT_3D ( 'NONE', #43987, #200499, #83070 ) ;
#210823=PLANE ( 'NONE',  #98285 ) ;
#210863=CARTESIAN_POINT ( 'NONE',  ( -16.77683809663752257, 12.41293291551535916, -211.2574046339461233 ) ) ;
#210898=VERTEX_POINT ( 'NONE', #65664 ) ;
#210972=CARTESIAN_POINT ( 'NONE',  ( -16.93294127766158752, 14.22806568586737264, -219.3218115319804156 ) ) ;
#211055=LINE ( 'NONE', #53264, #132618 ) ;
#211185=ORIENTED_EDGE ( 'NONE', *, *, #178228, .T. ) ;
#211332=CARTESIAN_POINT ( 'NONE',  ( -16.87331047859651179, 12.41403342719998726, -211.2428889513006993 ) ) ;
#211344=FACE_OUTER_BOUND ( 'NONE', #121014, .T. ) ;
#211429=AXIS2_PLACEMENT_3D ( 'NONE', #235198, #116538, #197336 ) ;
#211617=EDGE_CURVE ( 'NONE', #135298, #166393, #85541, .T. ) ;
#211749=CARTESIAN_POINT ( 'NONE',  ( -18.40000000000000213, 16.38400329561159907, -222.2501914957450424 ) ) ;
#212015=VERTEX_POINT ( 'NONE', #39310 ) ;
#212038=UNCERTAINTY_MEASURE_WITH_UNIT (LENGTH_MEASURE( 1.000000000000000082E-05 ), #230116, 'distance_accuracy_value', 'NONE');
#212269=CARTESIAN_POINT ( 'NONE',  ( -16.93826681692523195, 14.23933697485878902, -219.3352725080944481 ) ) ;
#212340=VERTEX_POINT ( 'NONE', #254034 ) ;
#212547=CARTESIAN_POINT ( 'NONE',  ( -16.97683809663752186, 13.99889777621145903, -218.5199410132753144 ) ) ;
#212572=EDGE_CURVE ( 'NONE', #203112, #190086, #47810, .T. ) ;
#213084=EDGE_CURVE ( 'NONE', #101456, #109830, #88542, .T. ) ;
#213103=CARTESIAN_POINT ( 'NONE',  ( 23.24999999999999645, 10.58889512527366428, -208.1606840254082158 ) ) ;
#213155=ORIENTED_EDGE ( 'NONE', *, *, #89203, .T. ) ;
#213571=EDGE_CURVE ( 'NONE', #175353, #223991, #215874, .T. ) ;
#213692=ORIENTED_EDGE ( 'NONE', *, *, #104637, .T. ) ;
#214009=FACE_OUTER_BOUND ( 'NONE', #91683, .T. ) ;
#214191=ADVANCED_FACE ( 'NONE', ( #136062 ), #233907, .F. ) ;
#214232=ORIENTED_EDGE ( 'NONE', *, *, #249232, .F. ) ;
#214249=ORIENTED_EDGE ( 'NONE', *, *, #49919, .F. ) ;
#214268=ORIENTED_EDGE ( 'NONE', *, *, #178252, .F. ) ;
#214276=COLOUR_RGB ( '', 0.40784314, 0.44705882, 0.49803922) ;
#214356=CARTESIAN_POINT ( 'NONE',  ( 18.39999999999999503, 15.64727632337704222, -218.9309421872099790 ) ) ;
#214474=AXIS2_PLACEMENT_3D ( 'NONE', #71317, #231669, #33493 ) ;
#214671=B_SPLINE_CURVE_WITH_KNOTS ( 'NONE', 3,
 ( #129756, #45086, #124628, #167625, #108903, #25536, #204142, #48928, #128478, #208031 ),
 .UNSPECIFIED., .F., .F.,
 ( 4, 2, 2, 2, 4 ),
 ( 0.000000000000000000, 0.0003916577441627133380, 0.0005874866162440714164, 0.0006854010522847114786, 0.0007833154883253517576 ),
 .UNSPECIFIED. ) ;
#214722=CARTESIAN_POINT ( 'NONE',  ( 15.15590539855245211, 12.47889858296947807, -214.0750992090277975 ) ) ;
#214748=VERTEX_POINT ( 'NONE', #157966 ) ;
#214767=EDGE_CURVE ( 'NONE', #182610, #244309, #101757, .T. ) ;
#214996=CARTESIAN_POINT ( 'NONE',  ( -16.77431908686105899, 12.41294867713261496, -211.2576179284957334 ) ) ;
#215151=PRODUCT_CONTEXT ( 'NONE', #83934, 'mechanical' ) ;
#215188=CARTESIAN_POINT ( 'NONE',  ( 12.30626653967340900, 12.80368220771249810, -215.8196253896158794 ) ) ;
#215302=ORIENTED_EDGE ( 'NONE', *, *, #201955, .T. ) ;
#215385=CARTESIAN_POINT ( 'NONE',  ( -21.64999999999999858, 14.25671114421267127, -219.2337924566137701 ) ) ;
#215564=DIRECTION ( 'NONE',  ( 1.073024830501117725E-15, -0.2128009952263604232, 0.9770955615653316162 ) ) ;
#215627=CARTESIAN_POINT ( 'NONE',  ( -17.04295772865507175, 14.23218548404114436, -219.2391338838992567 ) ) ;
#215811=CARTESIAN_POINT ( 'NONE',  ( 15.48841904831874849, 11.05741533749496242, -211.5383459065741647 ) ) ;
#215851=CARTESIAN_POINT ( 'NONE',  ( -18.40000000000000213, 16.35463830854640932, -222.1788605317357224 ) ) ;
#215874=CIRCLE ( 'NONE', #20282, 0.1999999999999987899 ) ;
#215888=ORIENTED_EDGE ( 'NONE', *, *, #19887, .F. ) ;
#215907=ADVANCED_FACE ( 'NONE', ( #147241 ), #195609, .T. ) ;
#215993=CARTESIAN_POINT ( 'NONE',  ( 12.84233041328156055, 12.47908687115373283, -214.0766389635194855 ) ) ;
#216053=ORIENTED_EDGE ( 'NONE', *, *, #59501, .T. ) ;
#216203=DIRECTION ( 'NONE',  ( 0.000000000000000000, 0.9770955615653313941, 0.2128009952263603677 ) ) ;
#216331=CARTESIAN_POINT ( 'NONE',  ( -14.23072895065542909, 12.43387192838033428, -213.6554569813165756 ) ) ;
#216409=LINE ( 'NONE', #37804, #96615 ) ;
#216600=CARTESIAN_POINT ( 'NONE',  ( -16.77431908686106254, 14.15188998083434235, -219.2421286581669335 ) ) ;
#216669=ORIENTED_EDGE ( 'NONE', *, *, #178627, .T. ) ;
#217314=DIRECTION ( 'NONE',  ( 0.000000000000000000, 0.9770955615653313941, 0.2128009952263603677 ) ) ;
#217382=LINE ( 'NONE', #177024, #130228 ) ;
#217402=ADVANCED_FACE ( 'NONE', ( #138975 ), #60742, .F. ) ;
#217549=CARTESIAN_POINT ( 'NONE',  ( -16.80891096016299002, 12.41027476423438891, -211.2256307007121734 ) ) ;
#217872=AXIS2_PLACEMENT_3D ( 'NONE', #29327, #205330, #26741 ) ;
#217875=VERTEX_POINT ( 'NONE', #83824 ) ;
#218136=CARTESIAN_POINT ( 'NONE',  ( -16.87683809663752399, 12.41403342719998726, -211.2428889513006993 ) ) ;
#218183=CARTESIAN_POINT ( 'NONE',  ( 20.99999999999999645, 13.96358247574307221, -219.2976327551816951 ) ) ;
#218250=B_SPLINE_CURVE_WITH_KNOTS ( 'NONE', 3,
 ( #100760, #154404, #233899, #122951, #184184, #44699, #26425, #86346, #61684, #124240, #102066, #5535, #241602 ),
 .UNSPECIFIED., .F., .F.,
 ( 4, 3, 3, 3, 4 ),
 ( -3.224855718277077941E-06, 0.000000000000000000, 6.199515528668320112E-06, 4.034952380127989350E-05, 7.452715123700383651E-05 ),
 .UNSPECIFIED. ) ;
#218275=ORIENTED_EDGE ( 'NONE', *, *, #214767, .T. ) ;
#218432=LINE ( 'NONE', #167188, #126231 ) ;
#218749=DIRECTION ( 'NONE',  ( 1.186688945009010077E-16, -0.9770955615653315052, -0.2128009952263603954 ) ) ;
#218890=CARTESIAN_POINT ( 'NONE',  ( -13.77178122865953469, 12.43384112479209591, -213.6551227491177940 ) ) ;
#219121=CARTESIAN_POINT ( 'NONE',  ( 23.04999999999999716, 11.31241850904329205, -211.4828089347303433 ) ) ;
#219185=CARTESIAN_POINT ( 'NONE',  ( -16.94107738177415712, 12.45552124806248706, -211.1315092113344463 ) ) ;
#219504=CARTESIAN_POINT ( 'NONE',  ( -16.77828822459933633, 14.15263002279597693, -219.2435359409537625 ) ) ;
#219513=FACE_OUTER_BOUND ( 'NONE', #142262, .T. ) ;
#219680=DIRECTION ( 'NONE',  ( 1.000000000000000000, 2.171475777237622503E-16, -9.970532993647777410E-16 ) ) ;
#219809=EDGE_LOOP ( 'NONE', ( #122936, #144816, #214249 ) ) ;
#219853=CARTESIAN_POINT ( 'NONE',  ( 13.43443725621852991, 12.44134409367007343, -213.7340784654985271 ) ) ;
#220047=COLOUR_RGB ( '', 0.40784314, 0.44705882, 0.49803922) ;
#220350=VERTEX_POINT ( 'NONE', #161939 ) ;
#220368=ORIENTED_EDGE ( 'NONE', *, *, #169195, .F. ) ;
#220497=VERTEX_POINT ( 'NONE', #93931 ) ;
#220760=AXIS2_PLACEMENT_3D ( 'NONE', #33964, #192997, #75631 ) ;
#220799=CARTESIAN_POINT ( 'NONE',  ( -16.77683809663752257, 14.15196434607590348, -219.2423291894720307 ) ) ;
#220856=EDGE_CURVE ( 'NONE', #233400, #190315, #136113, .T. ) ;
#220963=DIRECTION ( 'NONE',  ( -1.020425574104003999E-15, 0.2128009952263603677, -0.9770955615653313941 ) ) ;
#221212=EDGE_CURVE ( 'NONE', #142560, #104329, #183441, .T. ) ;
#221311=PLANE ( 'NONE',  #168624 ) ;
#221398=LINE ( 'NONE', #158910, #78429 ) ;
#221445=CARTESIAN_POINT ( 'NONE',  ( -15.75000000000000355, 12.70026017068886937, -215.3766613508543628 ) ) ;
#221460=LINE ( 'NONE', #63687, #11608 ) ;
#221594=DIRECTION ( 'NONE',  ( -0.000000000000000000, 0.2128009952263603677, -0.9770955615653313941 ) ) ;
#221626=ADVANCED_FACE ( 'NONE', ( #44911 ), #124453, .F. ) ;
#221710=CARTESIAN_POINT ( 'NONE',  ( -16.89935556175677078, 14.05479797069542514, -218.7766119553601527 ) ) ;
#221744=ORIENTED_EDGE ( 'NONE', *, *, #20926, .F. ) ;
#221795=ORIENTED_EDGE ( 'NONE', *, *, #143842, .T. ) ;
#221865=CARTESIAN_POINT ( 'NONE',  ( -16.87683809663752399, 12.47642768288813286, -211.9993005936843815 ) ) ;
#222051=EDGE_CURVE ( 'NONE', #167344, #76552, #211055, .T. ) ;
#222215=DIRECTION ( 'NONE',  ( -1.000000000000000000, -1.608698681449252075E-14, -3.503574203973550643E-15 ) ) ;
#222590=DIRECTION ( 'NONE',  ( 1.000000000000000000, 1.159508501126949290E-16, 2.525285885220369759E-17 ) ) ;
#222847=DIRECTION ( 'NONE',  ( -1.000000000000000000, 0.000000000000000000, 0.000000000000000000 ) ) ;
#223012=CARTESIAN_POINT ( 'NONE',  ( -16.87304349924914604, 14.17879107892816215, -219.2907450666499471 ) ) ;
#223125=EDGE_CURVE ( 'NONE', #106564, #209692, #194982, .T. ) ;
#223296=ORIENTED_EDGE ( 'NONE', *, *, #72082, .F. ) ;
#223403=DIRECTION ( 'NONE',  ( 1.000000000000000000, 0.000000000000000000, 0.000000000000000000 ) ) ;
#223510=FACE_OUTER_BOUND ( 'NONE', #115007, .T. ) ;
#223780=ADVANCED_FACE ( 'NONE', ( #117805 ), #52686, .F. ) ;
#223815=ORIENTED_EDGE ( 'NONE', *, *, #251024, .T. ) ;
#223928=EDGE_CURVE ( 'NONE', #15616, #3891, #141228, .T. ) ;
#223933=SURFACE_STYLE_FILL_AREA ( #244784 ) ;
#223991=VERTEX_POINT ( 'NONE', #45973 ) ;
#224045=VERTEX_POINT ( 'NONE', #48540 ) ;
#224157=CARTESIAN_POINT ( 'NONE',  ( -15.75000000000000355, 12.70026017068886937, -215.3766613508543628 ) ) ;
#224266=FACE_OUTER_BOUND ( 'NONE', #356, .T. ) ;
#224293=ORIENTED_EDGE ( 'NONE', *, *, #225405, .F. ) ;
#224337=EDGE_CURVE ( 'NONE', #106564, #224045, #46932, .T. ) ;
#224382=ORIENTED_EDGE ( 'NONE', *, *, #222051, .F. ) ;
#224701=ORIENTED_EDGE ( 'NONE', *, *, #253966, .T. ) ;
#225074=ORIENTED_EDGE ( 'NONE', *, *, #205978, .F. ) ;
#225405=EDGE_CURVE ( 'NONE', #208323, #25427, #139651, .T. ) ;
#225430=CARTESIAN_POINT ( 'NONE',  ( -14.22969084473442081, 13.17382239637292862, -217.0529139566851597 ) ) ;
#225568=CARTESIAN_POINT ( 'NONE',  ( -16.87036670365548474, 14.22508806334145959, -219.3732768077300932 ) ) ;
#225592=DIRECTION ( 'NONE',  ( 1.186688945009010077E-16, -0.9770955615653316162, -0.2128009952263604232 ) ) ;
#225732=CARTESIAN_POINT ( 'NONE',  ( -17.04761207306817994, 14.23370139713091120, -219.2388037341914071 ) ) ;
#226054=( BOUNDED_SURFACE ( )  B_SPLINE_SURFACE ( 3, 2, ( 
 ( #88952, #207655, #180697 ),
 ( #181978, #81553, #42454 ),
 ( #122003, #102397, #3309 ),
 ( #82832, #63297, #142817 ) ),
 .UNSPECIFIED., .F., .F., .F. ) 
 B_SPLINE_SURFACE_WITH_KNOTS ( ( 4, 4 ),
 ( 3, 3 ),
 ( 0.0008258556059633687975, 0.0009616864997632754760 ),
 ( 0.000000000000000000, 1.000000000000000000 ),
 .UNSPECIFIED. ) 
 GEOMETRIC_REPRESENTATION_ITEM ( )  RATIONAL_B_SPLINE_SURFACE ( (
 ( 1.000000000000000000, 0.9152888060719464036, 1.000000000000000000),
 ( 1.000000000000000000, 0.9327727094138169583, 1.000000000000000000),
 ( 1.000000000000000000, 0.9369023509258193050, 1.000000000000000000),
 ( 1.000000000000000000, 0.9246339933864469174, 1.000000000000000000) ) ) 
 REPRESENTATION_ITEM ( '' )  SURFACE ( )  );
#226230=SHAPE_REPRESENTATION_RELATIONSHIP ( 'NONE' , 'NONE' ,  #233377, #191218 ) ;
#226294=ORIENTED_EDGE ( 'NONE', *, *, #147720, .T. ) ;
#226490=CARTESIAN_POINT ( 'NONE',  ( -17.22361732159832215, 14.81732475420846207, -220.4208988007774224 ) ) ;
#226517=DIRECTION ( 'NONE',  ( 1.000000000000000000, 0.000000000000000000, 0.000000000000000000 ) ) ;
#226520=DIRECTION ( 'NONE',  ( 0.7071067811865456854, -0.6909108974501254608, -0.1504730267678059674 ) ) ;
#226539=ADVANCED_FACE ( 'NONE', ( #249721 ), #168944, .F. ) ;
#226673=DIRECTION ( 'NONE',  ( 0.000000000000000000, 0.9770955615653313941, 0.2128009952263603677 ) ) ;
#226718=ORIENTED_EDGE ( 'NONE', *, *, #223125, .T. ) ;
#226725=DIRECTION ( 'NONE',  ( 0.000000000000000000, 0.2128009952263603677, -0.9770955615653313941 ) ) ;
#226763=FACE_OUTER_BOUND ( 'NONE', #33999, .T. ) ;
#226778=CARTESIAN_POINT ( 'NONE',  ( -17.78241384942234049, 12.78794030309596330, -208.7042118961428514 ) ) ;
#226926=CARTESIAN_POINT ( 'NONE',  ( -33.72168855820452649, 13.17878477875124688, -207.5966336730521391 ) ) ;
#226997=CARTESIAN_POINT ( 'NONE',  ( -16.86379686415369861, 12.42092813644865501, -211.1560426965246791 ) ) ;
#227221=CARTESIAN_POINT ( 'NONE',  ( -17.05016517655962360, 12.41886358333906948, -211.2650670624473435 ) ) ;
#227263=CARTESIAN_POINT ( 'NONE',  ( -18.40000000000000213, 13.76412598303084778, -210.9488531877278206 ) ) ;
#227294=AXIS2_PLACEMENT_3D ( 'NONE', #14199, #93704, #74183 ) ;
#227387=ORIENTED_EDGE ( 'NONE', *, *, #223928, .F. ) ;
#227541=ADVANCED_FACE ( 'NONE', ( #30918 ), #32190, .F. ) ;
#227624=EDGE_LOOP ( 'NONE', ( #103930, #75897, #43360, #120091 ) ) ;
#227729=EDGE_CURVE ( 'NONE', #190086, #169179, #106301, .T. ) ;
#228024=CARTESIAN_POINT ( 'NONE',  ( -15.06720934482787300, 13.06253445771512922, -216.7219835687084810 ) ) ;
#228084=ORIENTED_EDGE ( 'NONE', *, *, #103318, .T. ) ;
#228171=CARTESIAN_POINT ( 'NONE',  ( 21.72449340488910607, 12.01681723992382800, -207.8496978137663689 ) ) ;
#228219=LINE ( 'NONE', #54372, #126918 ) ;
#228265=DIRECTION ( 'NONE',  ( -1.000000000000000000, 0.000000000000000000, 0.000000000000000000 ) ) ;
#228297=CARTESIAN_POINT ( 'NONE',  ( -16.87368910959167678, 12.41706751708832357, -211.2038420430882013 ) ) ;
#228686=ORIENTED_EDGE ( 'NONE', *, *, #185193, .T. ) ;
#229149=CARTESIAN_POINT ( 'NONE',  ( -16.77902162784673479, 12.41308644798263217, -211.2553675282883319 ) ) ;
#229263=CARTESIAN_POINT ( 'NONE',  ( -16.93344882324368683, 14.21793519637126124, -219.3067405467496371 ) ) ;
#229580=CARTESIAN_POINT ( 'NONE',  ( -16.86757978335471719, 12.41826068153812024, -211.1887541124544327 ) ) ;
#229613=CARTESIAN_POINT ( 'NONE',  ( -16.87383368123029825, 12.41403342719998371, -211.2428889513006993 ) ) ;
#229731=EDGE_CURVE ( 'NONE', #144652, #167344, #191693, .T. ) ;
#229791=FACE_OUTER_BOUND ( 'NONE', #129139, .T. ) ;
#229932=FACE_OUTER_BOUND ( 'NONE', #161560, .T. ) ;
#230116=( LENGTH_UNIT ( ) NAMED_UNIT ( * ) SI_UNIT ( .MILLI., .METRE. ) );
#230204=CARTESIAN_POINT ( 'NONE',  ( -18.40000000000000213, 15.59003939055400956, -218.9434077809016514 ) ) ;
#230340=CARTESIAN_POINT ( 'NONE',  ( -18.40000000000000213, 15.91777359887373500, -218.8720307647289758 ) ) ;
#230385=FACE_OUTER_BOUND ( 'NONE', #199170, .T. ) ;
#230462=CARTESIAN_POINT ( 'NONE',  ( 20.73486653747088937, 10.26442319175629692, -211.7110511407986735 ) ) ;
#230646=CARTESIAN_POINT ( 'NONE',  ( -17.29838795458583434, 12.55891772868854517, -209.9271805838396290 ) ) ;
#230735=CARTESIAN_POINT ( 'NONE',  ( -23.25000000000000355, 9.957490673325212427, -220.1701168356097469 ) ) ;
#230777=FACE_OUTER_BOUND ( 'NONE', #203228, .T. ) ;
#230892=CARTESIAN_POINT ( 'NONE',  ( -17.01825945287482966, 12.51174298335651791, -211.2216088517780292 ) ) ;
#231238=DIRECTION ( 'NONE',  ( 1.000000000000000000, 0.000000000000000000, 0.000000000000000000 ) ) ;
#231615=EDGE_CURVE ( 'NONE', #109830, #212015, #81006, .T. ) ;
#231669=DIRECTION ( 'NONE',  ( 0.7071067811865487940, 0.6909108974501225742, 0.1504730267678046074 ) ) ;
#231927=VERTEX_POINT ( 'NONE', #215385 ) ;
#231947=EDGE_CURVE ( 'NONE', #212340, #190315, #36793, .T. ) ;
#232329=ORIENTED_EDGE ( 'NONE', *, *, #98240, .F. ) ;
#232505=LINE ( 'NONE', #115102, #83839 ) ;
#232526=DIRECTION ( 'NONE',  ( 0.000000000000000000, -0.2128009952263603954, 0.9770955615653315052 ) ) ;
#232533=DIRECTION ( 'NONE',  ( -0.7071067811865475727, -0.6909108974501027012, -0.1504730267679016409 ) ) ;
#232584=CARTESIAN_POINT ( 'NONE',  ( 17.23472005113827876, 12.50908554981958076, -209.9975613761644979 ) ) ;
#232611=CARTESIAN_POINT ( 'NONE',  ( -18.36973785203555920, 16.37308737817262028, -222.2525688661744709 ) ) ;
#232639=CARTESIAN_POINT ( 'NONE',  ( 18.39999999999999503, 15.91777359887373500, -218.8720307647289758 ) ) ;
#232671=EDGE_LOOP ( 'NONE', ( #157465, #58257, #184158, #89652 ) ) ;
#232685=VECTOR ( 'NONE', #66367, 1000.000000000000227 ) ;
#232869=ORIENTED_EDGE ( 'NONE', *, *, #112597, .T. ) ;
#232894=UNCERTAINTY_MEASURE_WITH_UNIT (LENGTH_MEASURE( 1.000000000000000082E-05 ), #248402, 'distance_accuracy_value', 'NONE');
#233377=SHAPE_REPRESENTATION ( 'Snap Open Cable Crossbars 7', ( #2425 ), #135129 ) ;
#233400=VERTEX_POINT ( 'NONE', #2478 ) ;
#233491=CARTESIAN_POINT ( 'NONE',  ( 12.25000000000000355, 12.72457643131171423, -215.4883117230867811 ) ) ;
#233640=CARTESIAN_POINT ( 'NONE',  ( -16.94445028196808778, 12.44605341304038859, -211.1922452800140775 ) ) ;
#233745=EDGE_CURVE ( 'NONE', #169097, #96084, #191832, .T. ) ;
#233793=VERTEX_POINT ( 'NONE', #58288 ) ;
#233837=VERTEX_POINT ( 'NONE', #56993 ) ;
#233888=CIRCLE ( 'NONE', #250462, 0.09999999999999939493 ) ;
#233899=CARTESIAN_POINT ( 'NONE',  ( -16.94333152882355620, 14.20736394004534553, -219.2875565584338631 ) ) ;
#233907=PLANE ( 'NONE',  #211429 ) ;
#234129=ORIENTED_EDGE ( 'NONE', *, *, #77794, .T. ) ;
#234173=ORIENTED_EDGE ( 'NONE', *, *, #247251, .T. ) ;
#234279=CARTESIAN_POINT ( 'NONE',  ( 12.25000000000000000, 12.70026017068886937, -215.3766613508543628 ) ) ;
#234311=FACE_OUTER_BOUND ( 'NONE', #41123, .T. ) ;
#234564=CARTESIAN_POINT ( 'NONE',  ( -16.88783316861821859, 12.43579531710911290, -211.3428106928266743 ) ) ;
#234584=VERTEX_POINT ( 'NONE', #243747 ) ;
#234633=CARTESIAN_POINT ( 'NONE',  ( -18.40000000000000213, 13.19198836721619017, -207.5937580722650466 ) ) ;
#234706=LINE ( 'NONE', #174778, #138945 ) ;
#234719=DIRECTION ( 'NONE',  ( 1.186688945009009831E-16, -0.9770955615653316162, -0.2128009952263604232 ) ) ;
#234724=LINE ( 'NONE', #230892, #179567 ) ;
#234751=CARTESIAN_POINT ( 'NONE',  ( 15.74999999999999645, 12.70026017068886226, -215.3766613508543628 ) ) ;
#234856=DIRECTION ( 'NONE',  ( -1.000000000000000000, 0.000000000000000000, 0.000000000000000000 ) ) ;
#234865=EDGE_CURVE ( 'NONE', #171702, #15616, #198852, .T. ) ;
#234873=EDGE_LOOP ( 'NONE', ( #182337, #73268, #165046, #92217 ) ) ;
#235055=CARTESIAN_POINT ( 'NONE',  ( 18.39999999999997371, 16.37079970714665933, -222.2530670965321349 ) ) ;
#235123=ORIENTED_EDGE ( 'NONE', *, *, #148055, .F. ) ;
#235198=CARTESIAN_POINT ( 'NONE',  ( 23.24999999999999645, 13.44928205424795564, -207.5377222505711075 ) ) ;
#235341=CARTESIAN_POINT ( 'NONE',  ( -18.40000000000000213, 9.957490673325212427, -220.1701168356097469 ) ) ;
#235384=VERTEX_POINT ( 'NONE', #185414 ) ;
#235476=CIRCLE ( 'NONE', #227294, 1.749999999999999778 ) ;
#235519=CARTESIAN_POINT ( 'NONE',  ( 18.39999999999999503, 8.212522512469059066, -212.1579332307740344 ) ) ;
#235562=CARTESIAN_POINT ( 'NONE',  ( 12.29592348164038995, 12.60827992760467353, -214.9270390227368637 ) ) ;
#235769=CARTESIAN_POINT ( 'NONE',  ( -16.94226253665224391, 14.09585617079101461, -218.9651344997973581 ) ) ;
#235840=CARTESIAN_POINT ( 'NONE',  ( -16.77180007708459897, 12.41097209739636398, -211.2288325707822594 ) ) ;
#236076=EDGE_CURVE ( 'NONE', #212340, #209959, #168682, .T. ) ;
#236164=CARTESIAN_POINT ( 'NONE',  ( -16.80070461187863629, 14.15964768823248576, -219.2580391851904267 ) ) ;
#236188=CARTESIAN_POINT ( 'NONE',  ( -16.94037747912386038, 12.45507804527209927, -211.1327632053331627 ) ) ;
#236304=EDGE_CURVE ( 'NONE', #25427, #182610, #54251, .T. ) ;
#236641=ADVANCED_FACE ( 'NONE', ( #214009 ), #35404, .T. ) ;
#237001=DIRECTION ( 'NONE',  ( -1.073024830501117725E-15, 0.2128009952263603954, -0.9770955615653315052 ) ) ;
#237139=CARTESIAN_POINT ( 'NONE',  ( -16.82542659449979183, 12.41902688977936187, -211.3386554145826608 ) ) ;
#237389=LINE ( 'NONE', #139546, #140466 ) ;
#237456=CARTESIAN_POINT ( 'NONE',  ( 20.27550659511089037, 13.44185616693652996, -219.4112591824391529 ) ) ;
#237768=DIRECTION ( 'NONE',  ( 1.000000000000000000, 0.000000000000000000, 0.000000000000000000 ) ) ;
#237956=CARTESIAN_POINT ( 'NONE',  ( -16.97683809663752186, 13.90118822005492660, -218.5412211127979845 ) ) ;
#238018=ORIENTED_EDGE ( 'NONE', *, *, #28915, .T. ) ;
#238487=AXIS2_PLACEMENT_3D ( 'NONE', #120976, #105183, #184763 ) ;
#238600=FACE_OUTER_BOUND ( 'NONE', #149083, .T. ) ;
#238679=CARTESIAN_POINT ( 'NONE',  ( 20.27550659511089037, 11.69688800608038193, -211.3990755776034405 ) ) ;
#238734=CARTESIAN_POINT ( 'NONE',  ( -16.83233564386405590, 14.11297426559041845, -219.1366760747206399 ) ) ;
#238766=CARTESIAN_POINT ( 'NONE',  ( -16.93230518875208190, 12.44782693869981927, -211.1595675772403524 ) ) ;
#238968=ORIENTED_EDGE ( 'NONE', *, *, #120426, .F. ) ;
#239020=EDGE_LOOP ( 'NONE', ( #129926, #31791, #224701, #10700, #251567 ) ) ;
#239035=CARTESIAN_POINT ( 'NONE',  ( -16.27683809663750480, 13.59402435063957348, -219.4804627094287639 ) ) ;
#239106=VECTOR ( 'NONE', #57248, 1000.000000000000227 ) ;
#239447=ORIENTED_EDGE ( 'NONE', *, *, #50527, .F. ) ;
#239466=EDGE_CURVE ( 'NONE', #17273, #88954, #204261, .T. ) ;
#239529=LINE ( 'NONE', #242078, #84292 ) ;
#239567=DIRECTION ( 'NONE',  ( 0.000000000000000000, -0.9770955615653313941, -0.2128009952263603677 ) ) ;
#239625=FACE_OUTER_BOUND ( 'NONE', #191766, .T. ) ;
#239655=FACE_OUTER_BOUND ( 'NONE', #173176, .T. ) ;
#239727=CARTESIAN_POINT ( 'NONE',  ( -16.79814274880124358, 12.41384038458400063, -211.2454210646436650 ) ) ;
#239747=DIRECTION ( 'NONE',  ( -0.000000000000000000, 0.2128009952263603677, -0.9770955615653313941 ) ) ;
#239761=CARTESIAN_POINT ( 'NONE',  ( -13.12432614554023225, 12.45583213463953776, -213.8748143118951930 ) ) ;
#240326=VERTEX_POINT ( 'NONE', #250179 ) ;
#240383=CARTESIAN_POINT ( 'NONE',  ( -23.25000000000000355, 14.23543104469003673, -219.1360829004572395 ) ) ;
#240408=CARTESIAN_POINT ( 'NONE',  ( -23.25000000000000355, 16.64129698264336099, -222.1941556740511032 ) ) ;
#240563=VECTOR ( 'NONE', #217314, 1000.000000000000227 ) ;
#240566=EDGE_LOOP ( 'NONE', ( #226718, #199073, #9942, #65171 ) ) ;
#240836=VECTOR ( 'NONE', #63956, 1000.000000000000114 ) ;
#240861=CIRCLE ( 'NONE', #182433, 0.1000000000000054040 ) ;
#240916=CARTESIAN_POINT ( 'NONE',  ( -16.90138253750127362, 14.12954199452179616, -219.1198060924749029 ) ) ;
#241141=CARTESIAN_POINT ( 'NONE',  ( -16.77683809663752257, 14.15196434607590348, -219.2423291894720307 ) ) ;
#241273=AXIS2_PLACEMENT_3D ( 'NONE', #39331, #67526, #99258 ) ;
#241316=CARTESIAN_POINT ( 'NONE',  ( -16.88705144915432044, 14.09920906346404124, -218.9805296183471341 ) ) ;
#241359=LINE ( 'NONE', #197067, #143045 ) ;
#241453=LINE ( 'NONE', #61528, #150163 ) ;
#241466=CARTESIAN_POINT ( 'NONE',  ( -16.77683809663752257, 12.41293291551535916, -211.2574046339461233 ) ) ;
#241602=CARTESIAN_POINT ( 'NONE',  ( -16.89268316805465986, 14.16190809729244648, -219.2603268738197073 ) ) ;
#241662=EDGE_CURVE ( 'NONE', #22978, #100496, #21632, .T. ) ;
#241701=CARTESIAN_POINT ( 'NONE',  ( -23.25000000000000355, 12.53302308287915245, -211.3193184079345883 ) ) ;
#241723=CARTESIAN_POINT ( 'NONE',  ( -18.40000000000000213, 14.17280543801757986, -210.8598471598932349 ) ) ;
#241769=EDGE_LOOP ( 'NONE', ( #20696, #101704 ) ) ;
#241832=DIRECTION ( 'NONE',  ( 1.000000000000000000, 0.000000000000000000, 0.000000000000000000 ) ) ;
#242017=CARTESIAN_POINT ( 'NONE',  ( -17.22767730082070869, 14.82413144765285651, -220.4329393275840516 ) ) ;
#242078=CARTESIAN_POINT ( 'NONE',  ( -21.65000000000000213, 9.052352027203962592, -208.4953267290897543 ) ) ;
#242219=DIRECTION ( 'NONE',  ( -1.000000000000000000, -1.927470528863115795E-15, 0.000000000000000000 ) ) ;
#242619=DIRECTION ( 'NONE',  ( 0.5932847527679309119, -0.7865547670005531566, -0.1713032417725958989 ) ) ;
#242669=FACE_OUTER_BOUND ( 'NONE', #240566, .T. ) ;
#242716=AXIS2_PLACEMENT_3D ( 'NONE', #185350, #27599, #6707 ) ;
#242808=EDGE_LOOP ( 'NONE', ( #11396, #48237, #145024, #186361, #39344, #107200 ) ) ;
#242826=CARTESIAN_POINT ( 'NONE',  ( -16.90202395485563613, 12.41833139826750454, -211.1876964646075976 ) ) ;
#242891=DIRECTION ( 'NONE',  ( -0.000000000000000000, 0.2128009952263603677, -0.9770955615653313941 ) ) ;
#242969=VECTOR ( 'NONE', #99427, 1000.000000000000227 ) ;
#243013=AXIS2_PLACEMENT_3D ( 'NONE', #204567, #28557, #25946 ) ;
#243015=LINE ( 'NONE', #64394, #183336 ) ;
#243183=VECTOR ( 'NONE', #132659, 1000.000000000000227 ) ;
#243193=VECTOR ( 'NONE', #190176, 1000.000000000000000 ) ;
#243241=ORIENTED_EDGE ( 'NONE', *, *, #241662, .F. ) ;
#243316=CARTESIAN_POINT ( 'NONE',  ( -16.93658623642908267, 12.43561208657240513, -211.1991990270598478 ) ) ;
#243747=CARTESIAN_POINT ( 'NONE',  ( -16.94445028196808778, 12.44605341304038859, -211.1922452800140775 ) ) ;
#243956=CARTESIAN_POINT ( 'NONE',  ( -17.11825945287482753, 12.51174298335651791, -211.2216088517780292 ) ) ;
#244079=EDGE_CURVE ( 'NONE', #76552, #117708, #126063, .T. ) ;
#244309=VERTEX_POINT ( 'NONE', #152091 ) ;
#244425=FACE_OUTER_BOUND ( 'NONE', #8427, .T. ) ;
#244497=ORIENTED_EDGE ( 'NONE', *, *, #166969, .F. ) ;
#244784=FILL_AREA_STYLE ('',( #107850 ) ) ;
#244881=CARTESIAN_POINT ( 'NONE',  ( -12.25000000000000178, 12.65101141449786581, -215.1505311063239674 ) ) ;
#245140=ORIENTED_EDGE ( 'NONE', *, *, #82864, .F. ) ;
#245318=CARTESIAN_POINT ( 'NONE',  ( -16.83794237512073622, 12.42360805125251311, -211.3979450943548954 ) ) ;
#245375=ORIENTED_EDGE ( 'NONE', *, *, #93725, .T. ) ;
#245415=CARTESIAN_POINT ( 'NONE',  ( -16.86445178670658507, 12.41728787639459775, -211.2004468506748083 ) ) ;
#246063=VECTOR ( 'NONE', #20569, 1000.000000000000000 ) ;
#246253=LINE ( 'NONE', #67603, #77767 ) ;
#246541=CARTESIAN_POINT ( 'NONE',  ( -18.40000000000000213, 10.68101405709484197, -223.4922417449319028 ) ) ;
#246825=EDGE_CURVE ( 'NONE', #235384, #167344, #241453, .T. ) ;
#246924=AXIS2_PLACEMENT_3D ( 'NONE', #252985, #234719, #73110 ) ;
#247096=PRESENTATION_STYLE_ASSIGNMENT (( #11077 ) ) ;
#247251=EDGE_CURVE ( 'NONE', #142560, #171657, #234724, .T. ) ;
#247355=( NAMED_UNIT ( * ) PLANE_ANGLE_UNIT ( ) SI_UNIT ( $, .RADIAN. ) );
#247412=ORIENTED_EDGE ( 'NONE', *, *, #193394, .F. ) ;
#247603=CARTESIAN_POINT ( 'NONE',  ( -20.65000000000000568, 7.488999128699433072, -208.8358083214519070 ) ) ;
#247656=PLANE ( 'NONE',  #43468 ) ;
#247727=EDGE_CURVE ( 'NONE', #210119, #58804, #233888, .T. ) ;
#247879=LINE ( 'NONE', #9271, #126459 ) ;
#248145=STYLED_ITEM ( 'NONE', ( #247096 ), #191218 ) ;
#248402=( LENGTH_UNIT ( ) NAMED_UNIT ( * ) SI_UNIT ( .MILLI., .METRE. ) );
#248440=DIRECTION ( 'NONE',  ( 0.8049926720990052686, 0.5796958986739292330, 0.1262515858416406456 ) ) ;
#248521=AXIS2_PLACEMENT_3D ( 'NONE', #89001, #51146, #168611 ) ;
#248591=CARTESIAN_POINT ( 'NONE',  ( 21.13736287352038445, 10.55427114109327036, -211.6479253478778446 ) ) ;
#248875=CARTESIAN_POINT ( 'NONE',  ( -13.11924609551136101, 13.10551310878184061, -216.8535402360471949 ) ) ;
#248942=AXIS2_PLACEMENT_3D ( 'NONE', #240383, #176569, #199979 ) ;
#249232=EDGE_CURVE ( 'NONE', #35607, #149274, #124719, .T. ) ;
#249374=CARTESIAN_POINT ( 'NONE',  ( -17.11825945287483108, 12.41403342719999259, -211.2428889513006993 ) ) ;
#249721=FACE_OUTER_BOUND ( 'NONE', #98652, .T. ) ;
#249797=ADVANCED_FACE ( 'NONE', ( #229932 ), #90409, .F. ) ;
#250052=CARTESIAN_POINT ( 'NONE',  ( 18.39999999999999503, 16.64129698264336099, -222.1941556740511032 ) ) ;
#250165=ORIENTED_EDGE ( 'NONE', *, *, #81264, .T. ) ;
#250179=CARTESIAN_POINT ( 'NONE',  ( -20.65000000000000568, 8.212522512469059066, -212.1579332307740344 ) ) ;
#250284=LINE ( 'NONE', #230735, #90897 ) ;
#250462=AXIS2_PLACEMENT_3D ( 'NONE', #94887, #51896, #110610 ) ;
#250510=( BOUNDED_CURVE ( )  B_SPLINE_CURVE ( 3, ( #175209, #38228, #138560, #253404 ),
 .UNSPECIFIED., .F., .T. ) 
 B_SPLINE_CURVE_WITH_KNOTS ( ( 4, 4 ),
 ( 0.3000847527772380063, 0.5497968875596834781 ),
 .UNSPECIFIED. ) 
 CURVE ( )  GEOMETRIC_REPRESENTATION_ITEM ( )  RATIONAL_B_SPLINE_CURVE ( ( 1.000000000000000000, 0.9948104011409417691, 0.9948104011409417691, 1.000000000000000000 ) ) 
 REPRESENTATION_ITEM ( '' )  );
#250873=DIRECTION ( 'NONE',  ( 1.000000000000000000, 1.585864606265928695E-14, 4.552022003305584948E-15 ) ) ;
#250887=CARTESIAN_POINT ( 'NONE',  ( -23.25000000000000355, 13.44928205424795564, -207.5377222505711075 ) ) ;
#251024=EDGE_CURVE ( 'NONE', #69452, #251152, #179027, .T. ) ;
#251152=VERTEX_POINT ( 'NONE', #203687 ) ;
#251159=CARTESIAN_POINT ( 'NONE',  ( 21.13736287352038445, 9.830747757323642588, -208.3258004385557172 ) ) ;
#251300=CARTESIAN_POINT ( 'NONE',  ( -18.40000000000000213, 9.957490673325212427, -220.1701168356097469 ) ) ;
#251472=CARTESIAN_POINT ( 'NONE',  ( -16.94107738177415357, 12.45552124806248706, -211.1315092113344463 ) ) ;
#251567=ORIENTED_EDGE ( 'NONE', *, *, #58971, .F. ) ;
#251737=CARTESIAN_POINT ( 'NONE',  ( -16.89060415895971090, 12.41435804878020832, -211.2386428410039230 ) ) ;
#251748=CARTESIAN_POINT ( 'NONE',  ( 14.45963434102923451, 13.16206247923560291, -217.0199023716218676 ) ) ;
#251751=AXIS2_PLACEMENT_3D ( 'NONE', #29884, #109371, #149822 ) ;
#251906=B_SPLINE_CURVE_WITH_KNOTS ( 'NONE', 3,
 ( #220799, #182978, #78701, #219504, #137400, #98245, #59124, #3018, #158300, #1738 ),
 .UNSPECIFIED., .F., .F.,
 ( 4, 3, 3, 4 ),
 ( -2.000561356211570577E-06, 0.000000000000000000, 1.787822682428561198E-05, 4.206475347089817763E-05 ),
 .UNSPECIFIED. ) ;
#252160=LINE ( 'NONE', #232639, #52921 ) ;
#252183=DIRECTION ( 'NONE',  ( 1.000000000000000000, 3.854941057726231589E-15, 0.000000000000000000 ) ) ;
#252577=DIRECTION ( 'NONE',  ( -1.000000000000000000, 0.000000000000000000, 0.000000000000000000 ) ) ;
#252985=CARTESIAN_POINT ( 'NONE',  ( 13.99999999999999822, 13.18880795147152618, -215.2702608532411830 ) ) ;
#252990=DIRECTION ( 'NONE',  ( 1.000000000000000000, -0.000000000000000000, -0.000000000000000000 ) ) ;
#253011=CARTESIAN_POINT ( 'NONE',  ( -16.87036670365549895, 12.42497885867826390, -211.1079079717509046 ) ) ;
#253023=CARTESIAN_POINT ( 'NONE',  ( 15.39170923737820473, 12.96596579538267946, -216.4109158611323949 ) ) ;
#253059=ADVANCED_FACE ( 'NONE', ( #230385 ), #210823, .F. ) ;
#253361=STYLED_ITEM ( 'NONE', ( #187406 ), #20981 ) ;
#253404=CARTESIAN_POINT ( 'NONE',  ( -18.39999999999999858, 13.19494617735151465, -207.6708402378485516 ) ) ;
#253492=ORIENTED_EDGE ( 'NONE', *, *, #227729, .F. ) ;
#253846=ORIENTED_EDGE ( 'NONE', *, *, #63243, .T. ) ;
#253966=EDGE_CURVE ( 'NONE', #234584, #204749, #80801, .T. ) ;
#254034=CARTESIAN_POINT ( 'NONE',  ( -16.81744102076748959, 14.15900158805613884, -219.2550725561364118 ) ) ;
#254049=CARTESIAN_POINT ( 'NONE',  ( -23.25000000000000355, 8.212522512469059066, -212.1579332307740344 ) ) ;
#254115=CARTESIAN_POINT ( 'NONE',  ( -16.92280123533699054, 12.45672818331194520, -211.4389258949002226 ) ) ;
#254161=ORIENTED_EDGE ( 'NONE', *, *, #112597, .F. ) ;
#254666=CARTESIAN_POINT ( 'NONE',  ( -18.34374000495059676, 16.37079970714665933, -222.2530670965321349 ) ) ;
#254730=ORIENTED_EDGE ( 'NONE', *, *, #205105, .F. ) ;
#254883=ADVANCED_FACE ( 'NONE', ( #172454 ), #9476, .F. ) ;
#255282=CARTESIAN_POINT ( 'NONE',  ( -16.81744102076748959, 14.15900158805613884, -219.2550725561364118 ) ) ;
#255347=ORIENTED_EDGE ( 'NONE', *, *, #78419, .T. ) ;
#255542=CYLINDRICAL_SURFACE ( 'NONE', #173214, 0.9000000000000014655 ) ;
#255621=CARTESIAN_POINT ( 'NONE',  ( -23.25000000000000355, 8.212522512469059066, -212.1579332307740344 ) ) ;
#255710=CARTESIAN_POINT ( 'NONE',  ( -16.93226657140833069, 12.44727255555560319, -211.1626918736521361 ) ) ;
#255720=EDGE_CURVE ( 'NONE', #186535, #55330, #11456, .T. ) ;
#256009=LINE ( 'NONE', #59110, #98221 ) ;
#256045=CARTESIAN_POINT ( 'NONE',  ( 20.27550659511088682, 10.97336462231075416, -208.0769506682813130 ) ) ;
#256124=ORIENTED_EDGE ( 'NONE', *, *, #58664, .T. ) ;
#256354=CARTESIAN_POINT ( 'NONE',  ( 14.56326696814969957, 12.44126776692609582, -213.7332981774226539 ) ) ;
#256385=CARTESIAN_POINT ( 'NONE',  ( -21.65000000000000213, 9.052352027203962592, -208.4953267290897543 ) ) ;
#256638=CARTESIAN_POINT ( 'NONE',  ( -16.87683809663752399, 12.47642768288814707, -211.9993005936845805 ) ) ;
#256697=CARTESIAN_POINT ( 'NONE',  ( -15.75000000000001066, 12.65163926562330765, -215.1534139431610413 ) ) ;
#256790=CARTESIAN_POINT ( 'NONE',  ( 12.25000000000000000, 13.18880795147152618, -215.2702608532411830 ) ) ;
#256822=CARTESIAN_POINT ( 'NONE',  ( 14.22916352759893321, 13.17759476088265380, -217.0636392655389670 ) ) ;
#256973=ORIENTED_EDGE ( 'NONE', *, *, #148055, .T. ) ;
#256987=CIRCLE ( 'NONE', #144593, 1.500000000000001332 ) ;
#257002=DIRECTION ( 'NONE',  ( -1.000000000000000000, 0.000000000000000000, 0.000000000000000000 ) ) ;
#257275=EDGE_LOOP ( 'NONE', ( #8386, #125288, #208022, #169387, #175284, #78412 ) ) ;
#257507=CARTESIAN_POINT ( 'NONE',  ( -17.78043020864321022, 15.53411659463512429, -221.3228573289305245 ) ) ;
#257657=CARTESIAN_POINT ( 'NONE',  ( 18.39999999999998082, 13.17878477875124865, -207.5966336730521391 ) ) ;
#258040=LINE ( 'NONE', #39065, #116708 ) ;
ENDSEC;
END-ISO-10303-21;
